ISO-10303-21;
HEADER;
/* Generated by software containing ST-Developer
 * from STEP Tools, Inc. (www.steptools.com) 
 */

FILE_DESCRIPTION(
/* description */ ('Independent two-stage semi-open centrifugal-pump CAD. Shared impeller
s, open-machinable return casings, removable diaphragms, bronze wear/j
ournal rings, volume-preserving seal instances, retained keyed shaft, 
opposed mechanical face rings and partly threaded tie hardware. Native
 shaft rotation. Geometric topology/clearance only; flow/head/efficien
cy, pressure, cavitation, balance, preload, face loading and secondary
 seal fits/bonds, material/thermal/tolerance selection and life unassi
gned. External drive, coupling, anchors and piping bolts omitted.'),
/* implementation_level */ '2;1');

FILE_NAME(
/* name */ 'Socket head tie bolt M6x136.step',
/* time_stamp */ '2026-11-08T18:06:32-08:00',
/* author */ (''),
/* organization */ (''),
/* preprocessor_version */ 'ST-DEVELOPER v20.2',
/* originating_system */ 'Autodesk Translation Framework v15.17.0.0',
/* authorisation */ '');

FILE_SCHEMA (('AUTOMOTIVE_DESIGN { 1 0 10303 214 3 1 1 }'));
ENDSEC;

DATA;
#10=MECHANICAL_DESIGN_GEOMETRIC_PRESENTATION_REPRESENTATION('',(#411),#16687);
#135=CONICAL_SURFACE('',#6937,0.25,0.78539816339745);
#146=B_SPLINE_SURFACE_WITH_KNOTS('',3,3,((#15976,#15977,#15978,#15979,#15980,
#15981,#15982,#15983,#15984,#15985,#15986,#15987,#15988,#15989,#15990,#15991,
#15992,#15993,#15994,#15995,#15996,#15997,#15998,#15999,#16000,#16001,#16002,
#16003,#16004,#16005,#16006,#16007,#16008,#16009,#16010,#16011,#16012,#16013,
#16014,#16015,#16016,#16017,#16018,#16019,#16020,#16021,#16022,#16023,#16024,
#16025,#16026),(#16027,#16028,#16029,#16030,#16031,#16032,#16033,#16034,
#16035,#16036,#16037,#16038,#16039,#16040,#16041,#16042,#16043,#16044,#16045,
#16046,#16047,#16048,#16049,#16050,#16051,#16052,#16053,#16054,#16055,#16056,
#16057,#16058,#16059,#16060,#16061,#16062,#16063,#16064,#16065,#16066,#16067,
#16068,#16069,#16070,#16071,#16072,#16073,#16074,#16075,#16076,#16077),
(#16078,#16079,#16080,#16081,#16082,#16083,#16084,#16085,#16086,#16087,
#16088,#16089,#16090,#16091,#16092,#16093,#16094,#16095,#16096,#16097,#16098,
#16099,#16100,#16101,#16102,#16103,#16104,#16105,#16106,#16107,#16108,#16109,
#16110,#16111,#16112,#16113,#16114,#16115,#16116,#16117,#16118,#16119,#16120,
#16121,#16122,#16123,#16124,#16125,#16126,#16127,#16128),(#16129,#16130,
#16131,#16132,#16133,#16134,#16135,#16136,#16137,#16138,#16139,#16140,#16141,
#16142,#16143,#16144,#16145,#16146,#16147,#16148,#16149,#16150,#16151,#16152,
#16153,#16154,#16155,#16156,#16157,#16158,#16159,#16160,#16161,#16162,#16163,
#16164,#16165,#16166,#16167,#16168,#16169,#16170,#16171,#16172,#16173,#16174,
#16175,#16176,#16177,#16178,#16179)),.UNSPECIFIED.,.F.,.F.,.F.,(4,4),(4,
1,1,1,1,1,1,1,1,1,1,1,1,1,1,1,1,1,1,1,1,1,1,1,1,1,1,1,1,1,1,1,1,1,1,1,1,
1,1,1,1,1,1,1,1,1,1,1,4),(0.,0.0658467982010765),(11.6150328478183,12.6135684378078,
13.6121040277972,14.6106396177866,15.609175207776,16.6077107977655,17.6062463877549,
18.6047819777443,19.6033175677338,20.6018531577232,21.6003887477126,22.5989243377021,
23.5974599276915,24.5959955176809,25.5945311076704,26.5930666976598,27.5916022876492,
28.5901378776387,29.5886734676281,30.5872090576175,31.585744647607,32.5842802375964,
33.5828158275858,34.5813514175752,35.5798870075647,36.5784225975541,37.5769581875435,
38.575493777533,39.5740293675224,40.5725649575118,41.5711005475013,42.5696361374907,
43.5681717274801,44.5667073174696,45.565242907459,46.5637784974484,47.5623140874379,
48.5608496774273,49.5593852674167,50.5579208574061,51.5564564473956,52.554992037385,
53.5535276273744,54.5520632173639,55.5505988073533,56.5491343973427,57.5476699873322,
58.5462055773216,59.544741167311),.UNSPECIFIED.);
#147=B_SPLINE_SURFACE_WITH_KNOTS('',3,3,((#16278,#16279,#16280,#16281,#16282,
#16283,#16284,#16285,#16286,#16287,#16288,#16289,#16290,#16291,#16292,#16293,
#16294,#16295,#16296,#16297,#16298,#16299,#16300,#16301,#16302,#16303,#16304,
#16305,#16306,#16307,#16308,#16309,#16310,#16311,#16312,#16313,#16314,#16315,
#16316,#16317,#16318,#16319,#16320,#16321,#16322,#16323,#16324,#16325,#16326,
#16327,#16328,#16329,#16330),(#16331,#16332,#16333,#16334,#16335,#16336,
#16337,#16338,#16339,#16340,#16341,#16342,#16343,#16344,#16345,#16346,#16347,
#16348,#16349,#16350,#16351,#16352,#16353,#16354,#16355,#16356,#16357,#16358,
#16359,#16360,#16361,#16362,#16363,#16364,#16365,#16366,#16367,#16368,#16369,
#16370,#16371,#16372,#16373,#16374,#16375,#16376,#16377,#16378,#16379,#16380,
#16381,#16382,#16383),(#16384,#16385,#16386,#16387,#16388,#16389,#16390,
#16391,#16392,#16393,#16394,#16395,#16396,#16397,#16398,#16399,#16400,#16401,
#16402,#16403,#16404,#16405,#16406,#16407,#16408,#16409,#16410,#16411,#16412,
#16413,#16414,#16415,#16416,#16417,#16418,#16419,#16420,#16421,#16422,#16423,
#16424,#16425,#16426,#16427,#16428,#16429,#16430,#16431,#16432,#16433,#16434,
#16435,#16436),(#16437,#16438,#16439,#16440,#16441,#16442,#16443,#16444,
#16445,#16446,#16447,#16448,#16449,#16450,#16451,#16452,#16453,#16454,#16455,
#16456,#16457,#16458,#16459,#16460,#16461,#16462,#16463,#16464,#16465,#16466,
#16467,#16468,#16469,#16470,#16471,#16472,#16473,#16474,#16475,#16476,#16477,
#16478,#16479,#16480,#16481,#16482,#16483,#16484,#16485,#16486,#16487,#16488,
#16489)),.UNSPECIFIED.,.F.,.F.,.F.,(4,4),(4,1,1,1,1,1,1,1,1,1,1,1,1,1,1,
1,1,1,1,1,1,1,1,1,1,1,1,1,1,1,1,1,1,1,1,1,1,1,1,1,1,1,1,1,1,1,1,1,1,1,4),
(0.,0.0658467982010765),(8.307477552401,9.30744448228904,10.3074114121771,
11.3073783420651,12.3073452719531,13.3073122018412,14.3072791317292,15.3072460616173,
16.3072129915053,17.3071799213933,18.3071468512814,19.3071137811694,20.3070807110574,
21.3070476409455,22.3070145708335,23.3069815007215,24.3069484306096,25.3069153604976,
26.3068822903856,27.3068492202737,28.3068161501617,29.3067830800498,30.3067500099378,
31.3067169398258,32.3066838697139,33.3066507996019,34.3066177294899,35.306584659378,
36.306551589266,37.306518519154,38.3064854490421,39.3064523789301,40.3064193088181,
41.3063862387062,42.3063531685942,43.3063200984823,44.3062870283703,45.3062539582583,
46.3062208881464,47.3061878180344,48.3061547479224,49.3061216778105,50.3060886076985,
51.3060555375865,52.3060224674746,53.3059893973626,54.3059563272507,55.3059232571387,
56.3058901870267,57.3058571169148,58.3058240468028),.UNSPECIFIED.);
#318=B_SPLINE_CURVE_WITH_KNOTS('',3,(#15280,#15281,#15282,#15283,#15284,
#15285,#15286,#15287,#15288,#15289),.UNSPECIFIED.,.F.,.F.,(4,3,3,4),(-4.09293042013064,
-3.99414235995773,-2.99560676996829,-2.0686381749092),.UNSPECIFIED.);
#319=B_SPLINE_CURVE_WITH_KNOTS('',3,(#15297,#15298,#15299,#15300,#15301,
#15302,#15303),.UNSPECIFIED.,.F.,.F.,(4,3,4),(0.,0.999966929888035,1.11730040836829),
 .UNSPECIFIED.);
#320=B_SPLINE_CURVE_WITH_KNOTS('',3,(#15308,#15309,#15310,#15311,#15312,
#15313,#15314,#15315,#15316,#15317,#15318,#15319,#15320,#15321,#15322,#15323,
#15324,#15325,#15326,#15327,#15328,#15329),.UNSPECIFIED.,.F.,.F.,(4,3,3,
3,3,3,3,4),(-10.3761157273102,-9.98535589989431,-8.98682030990488,-7.98828471991545,
-6.98974912992602,-5.99121353993659,-4.99267794994716,-4.09293042013064),
 .UNSPECIFIED.);
#321=B_SPLINE_CURVE_WITH_KNOTS('',3,(#15330,#15331,#15332,#15333,#15334,
#15335,#15336,#15337,#15338,#15339,#15340,#15341,#15342,#15343,#15344,#15345,
#15346,#15347,#15348,#15349,#15350,#15351),.UNSPECIFIED.,.F.,.F.,(4,3,3,
3,3,3,3,4),(1.11730040836829,1.99993385977607,2.99990078966411,3.99986771955214,
4.99983464944018,5.99980157932822,6.99976850921625,7.40048571554796),
 .UNSPECIFIED.);
#322=B_SPLINE_CURVE_WITH_KNOTS('',3,(#15356,#15357,#15358,#15359,#15360,
#15361,#15362,#15363,#15364,#15365,#15366,#15367,#15368,#15369,#15370,#15371,
#15372,#15373,#15374,#15375,#15376,#15377),.UNSPECIFIED.,.F.,.F.,(4,3,3,
3,3,3,3,4),(-16.6593010344898,-15.9765694398309,-14.9780338498415,-13.979498259852,
-12.9809626698626,-11.9824270798732,-10.9838914898837,-10.3761157273102),
 .UNSPECIFIED.);
#323=B_SPLINE_CURVE_WITH_KNOTS('',3,(#15378,#15379,#15380,#15381,#15382,
#15383,#15384,#15385,#15386,#15387,#15388,#15389,#15390,#15391,#15392,#15393,
#15394,#15395,#15396,#15397,#15398,#15399),.UNSPECIFIED.,.F.,.F.,(4,3,3,
3,3,3,3,4),(7.40048571554796,7.99973543910429,8.99970236899232,9.99966929888036,
10.9996362287684,11.9996031586564,12.9995700885445,13.6836710227275),
 .UNSPECIFIED.);
#324=B_SPLINE_CURVE_WITH_KNOTS('',3,(#15404,#15405,#15406,#15407,#15408,
#15409,#15410,#15411,#15412,#15413,#15414,#15415,#15416,#15417,#15418,#15419,
#15420,#15421,#15422,#15423,#15424,#15425),.UNSPECIFIED.,.F.,.F.,(4,3,3,
3,3,3,3,4),(-22.9424863416693,-21.9677829797675,-20.9692473897781,-19.9707117997886,
-18.9721762097992,-17.9736406198098,-16.9751050298203,-16.6593010344898),
 .UNSPECIFIED.);
#325=B_SPLINE_CURVE_WITH_KNOTS('',3,(#15426,#15427,#15428,#15429,#15430,
#15431,#15432,#15433,#15434,#15435,#15436,#15437,#15438,#15439,#15440,#15441,
#15442,#15443,#15444,#15445,#15446,#15447),.UNSPECIFIED.,.F.,.F.,(4,3,3,
3,3,3,3,4),(13.6836710227275,13.9995370184325,14.9995039483205,15.9994708782086,
16.9994378080966,17.9994047379846,18.9993716678727,19.9668563299071),
 .UNSPECIFIED.);
#326=B_SPLINE_CURVE_WITH_KNOTS('',3,(#15452,#15453,#15454,#15455,#15456,
#15457,#15458,#15459,#15460,#15461,#15462,#15463,#15464,#15465,#15466,#15467,
#15468,#15469,#15470,#15471,#15472,#15473,#15474,#15475,#15476),
 .UNSPECIFIED.,.F.,.F.,(4,3,3,3,3,3,3,3,4),(-29.225671648849,-28.9575321096935,
-27.9589965197041,-26.9604609297146,-25.9619253397252,-24.9633897497358,
-23.9648541597464,-22.9663185697569,-22.9424863416693),.UNSPECIFIED.);
#327=B_SPLINE_CURVE_WITH_KNOTS('',3,(#15477,#15478,#15479,#15480,#15481,
#15482,#15483,#15484,#15485,#15486,#15487,#15488,#15489,#15490,#15491,#15492,
#15493,#15494,#15495,#15496,#15497,#15498,#15499,#15500,#15501),
 .UNSPECIFIED.,.F.,.F.,(4,3,3,3,3,3,3,3,4),(19.9668563299071,19.9993385977607,
20.9993055276488,21.9992724575368,22.9992393874248,23.9992063173129,24.9991732472009,
25.9991401770889,26.2500416370867),.UNSPECIFIED.);
#328=B_SPLINE_CURVE_WITH_KNOTS('',3,(#15506,#15507,#15508,#15509,#15510,
#15511,#15512,#15513,#15514,#15515,#15516,#15517,#15518,#15519,#15520,#15521,
#15522,#15523,#15524,#15525,#15526,#15527),.UNSPECIFIED.,.F.,.F.,(4,3,3,
3,3,3,3,4),(-35.5088569560286,-34.9487456496301,-33.9502100596407,-32.9516744696512,
-31.9531388796618,-30.9546032896724,-29.9560676996829,-29.225671648849),
 .UNSPECIFIED.);
#329=B_SPLINE_CURVE_WITH_KNOTS('',3,(#15528,#15529,#15530,#15531,#15532,
#15533,#15534,#15535,#15536,#15537,#15538,#15539,#15540,#15541,#15542,#15543,
#15544,#15545,#15546,#15547,#15548,#15549),.UNSPECIFIED.,.F.,.F.,(4,3,3,
3,3,3,3,4),(26.2500416370867,26.999107106977,27.999074036865,28.999040966753,
29.9990078966411,30.9989748265291,31.9989417564172,32.5332269442662),
 .UNSPECIFIED.);
#330=B_SPLINE_CURVE_WITH_KNOTS('',3,(#15554,#15555,#15556,#15557,#15558,
#15559,#15560,#15561,#15562,#15563,#15564,#15565,#15566,#15567,#15568,#15569,
#15570,#15571,#15572,#15573,#15574,#15575),.UNSPECIFIED.,.F.,.F.,(4,3,3,
3,3,3,3,4),(-41.7920422632081,-40.9399591895667,-39.9414235995773,-38.9428880095878,
-37.9443524195984,-36.945816829609,-35.9472812396195,-35.5088569560286),
 .UNSPECIFIED.);
#331=B_SPLINE_CURVE_WITH_KNOTS('',3,(#15576,#15577,#15578,#15579,#15580,
#15581,#15582,#15583,#15584,#15585,#15586,#15587,#15588,#15589,#15590,#15591,
#15592,#15593,#15594,#15595,#15596,#15597),.UNSPECIFIED.,.F.,.F.,(4,3,3,
3,3,3,3,4),(32.5332269442662,32.9989086863052,33.9988756161932,34.9988425460813,
35.9988094759693,36.9987764058573,37.9987433357454,38.8164122514459),
 .UNSPECIFIED.);
#332=B_SPLINE_CURVE_WITH_KNOTS('',3,(#15603,#15604,#15605,#15606,#15607,
#15608,#15609,#15610,#15611,#15612),.UNSPECIFIED.,.F.,.F.,(4,1,1,1,1,1,
1,4),(53.4070751110265,53.5535276273744,54.5520632173639,55.5505988073533,
56.5491343973427,57.5476699873322,58.5462055773216,59.544741167311),
 .UNSPECIFIED.);
#333=B_SPLINE_CURVE_WITH_KNOTS('',3,(#15615,#15616,#15617,#15618,#15619,
#15620,#15621,#15622),.UNSPECIFIED.,.F.,.F.,(4,1,1,1,1,4),(53.4070751110265,
54.3059563272507,55.3059232571387,56.3058901870267,57.3058571169148,58.3058240468028),
 .UNSPECIFIED.);
#334=B_SPLINE_CURVE_WITH_KNOTS('',3,(#15627,#15628,#15629,#15630,#15631,
#15632,#15633,#15634,#15635,#15636),.UNSPECIFIED.,.F.,.F.,(4,1,1,1,1,1,
1,4),(47.1238898038469,47.5623140874379,48.5608496774273,49.5593852674167,
50.5579208574061,51.5564564473956,52.554992037385,53.4070751110265),
 .UNSPECIFIED.);
#335=B_SPLINE_CURVE_WITH_KNOTS('',3,(#15637,#15638,#15639,#15640,#15641,
#15642,#15643,#15644,#15645,#15646,#15647),.UNSPECIFIED.,.F.,.F.,(4,1,1,
1,1,1,1,1,4),(47.1238898038469,47.3061878180344,48.3061547479224,49.3061216778105,
50.3060886076985,51.3060555375865,52.3060224674746,53.3059893973626,53.4070751110265),
 .UNSPECIFIED.);
#336=B_SPLINE_CURVE_WITH_KNOTS('',3,(#15652,#15653,#15654,#15655,#15656,
#15657,#15658,#15659,#15660,#15661),.UNSPECIFIED.,.F.,.F.,(4,1,1,1,1,1,
1,4),(40.8407044966673,41.5711005475013,42.5696361374907,43.5681717274801,
44.5667073174696,45.565242907459,46.5637784974484,47.1238898038469),
 .UNSPECIFIED.);
#337=B_SPLINE_CURVE_WITH_KNOTS('',3,(#15662,#15663,#15664,#15665,#15666,
#15667,#15668,#15669,#15670,#15671),.UNSPECIFIED.,.F.,.F.,(4,1,1,1,1,1,
1,4),(40.8407044966673,41.3063862387062,42.3063531685942,43.3063200984823,
44.3062870283703,45.3062539582583,46.3062208881464,47.1238898038469),
 .UNSPECIFIED.);
#338=B_SPLINE_CURVE_WITH_KNOTS('',3,(#15676,#15677,#15678,#15679,#15680,
#15681,#15682,#15683,#15684,#15685,#15686),.UNSPECIFIED.,.F.,.F.,(4,1,1,
1,1,1,1,1,4),(34.5575191894877,34.5813514175752,35.5798870075647,36.5784225975541,
37.5769581875435,38.575493777533,39.5740293675224,40.5725649575118,40.8407044966673),
 .UNSPECIFIED.);
#339=B_SPLINE_CURVE_WITH_KNOTS('',3,(#15687,#15688,#15689,#15690,#15691,
#15692,#15693,#15694,#15695,#15696),.UNSPECIFIED.,.F.,.F.,(4,1,1,1,1,1,
1,4),(34.5575191894877,35.306584659378,36.306551589266,37.306518519154,
38.3064854490421,39.3064523789301,40.3064193088181,40.8407044966673),
 .UNSPECIFIED.);
#340=B_SPLINE_CURVE_WITH_KNOTS('',3,(#15701,#15702,#15703,#15704,#15705,
#15706,#15707,#15708,#15709,#15710),.UNSPECIFIED.,.F.,.F.,(4,1,1,1,1,1,
1,4),(28.2743338823081,28.5901378776387,29.5886734676281,30.5872090576175,
31.585744647607,32.5842802375964,33.5828158275858,34.5575191894877),
 .UNSPECIFIED.);
#341=B_SPLINE_CURVE_WITH_KNOTS('',3,(#15711,#15712,#15713,#15714,#15715,
#15716,#15717,#15718,#15719,#15720,#15721),.UNSPECIFIED.,.F.,.F.,(4,1,1,
1,1,1,1,1,4),(28.2743338823081,28.3068161501617,29.3067830800498,30.3067500099378,
31.3067169398258,32.3066838697139,33.3066507996019,34.3066177294899,34.5575191894877),
 .UNSPECIFIED.);
#342=B_SPLINE_CURVE_WITH_KNOTS('',3,(#15726,#15727,#15728,#15729,#15730,
#15731,#15732,#15733,#15734,#15735),.UNSPECIFIED.,.F.,.F.,(4,1,1,1,1,1,
1,4),(21.9911485751285,22.5989243377021,23.5974599276915,24.5959955176809,
25.5945311076704,26.5930666976598,27.5916022876492,28.2743338823081),
 .UNSPECIFIED.);
#343=B_SPLINE_CURVE_WITH_KNOTS('',3,(#15736,#15737,#15738,#15739,#15740,
#15741,#15742,#15743,#15744,#15745),.UNSPECIFIED.,.F.,.F.,(4,1,1,1,1,1,
1,4),(21.9911485751285,22.3070145708335,23.3069815007215,24.3069484306096,
25.3069153604976,26.3068822903856,27.3068492202737,28.2743338823081),
 .UNSPECIFIED.);
#344=B_SPLINE_CURVE_WITH_KNOTS('',3,(#15750,#15751,#15752,#15753,#15754,
#15755,#15756,#15757,#15758,#15759),.UNSPECIFIED.,.F.,.F.,(4,1,1,1,1,1,
1,4),(15.707963267949,16.6077107977655,17.6062463877549,18.6047819777443,
19.6033175677338,20.6018531577232,21.6003887477126,21.9911485751285),
 .UNSPECIFIED.);
#345=B_SPLINE_CURVE_WITH_KNOTS('',3,(#15760,#15761,#15762,#15763,#15764,
#15765,#15766,#15767,#15768,#15769),.UNSPECIFIED.,.F.,.F.,(4,1,1,1,1,1,
1,4),(15.707963267949,16.3072129915053,17.3071799213933,18.3071468512814,
19.3071137811694,20.3070807110574,21.3070476409455,21.9911485751285),
 .UNSPECIFIED.);
#346=B_SPLINE_CURVE_WITH_KNOTS('',3,(#15772,#15773,#15774,#15775,#15776,
#15777,#15778,#15779,#15780,#15781,#15782,#15783,#15784,#15785,#15786,#15787,
#15788,#15789,#15790,#15791,#15792,#15793,#15794,#15795,#15796,#15797,#15798,
#15799,#15800,#15801,#15802,#15803,#15804,#15805,#15806,#15807,#15808,#15809,
#15810,#15811,#15812,#15813,#15814,#15815,#15816,#15817,#15818,#15819,#15820,
#15821,#15822,#15823,#15824,#15825,#15826,#15827,#15828,#15829,#15830,#15831,
#15832,#15833,#15834,#15835,#15836,#15837,#15838,#15839,#15840,#15841,#15842,
#15843,#15844,#15845,#15846,#15847,#15848,#15849,#15850,#15851,#15852,#15853,
#15854,#15855,#15856,#15857,#15858,#15859,#15860,#15861,#15862,#15863,#15864,
#15865,#15866,#15867,#15868,#15869,#15870,#15871,#15872,#15873,#15874,#15875,
#15876,#15877,#15878,#15879,#15880,#15881,#15882,#15883,#15884,#15885,#15886,
#15887,#15888,#15889,#15890,#15891,#15892,#15893,#15894,#15895,#15896,#15897,
#15898,#15899,#15900,#15901,#15902,#15903,#15904,#15905,#15906,#15907,#15908,
#15909,#15910),.UNSPECIFIED.,.F.,.F.,(4,3,3,3,3,3,3,3,3,3,3,3,3,3,3,3,3,
3,3,3,3,3,3,3,3,3,3,3,3,3,3,3,3,3,3,3,3,3,3,3,3,3,3,3,3,3,4),(-1.51155304937198,
-1.46675125746741,-1.44534760943282,-1.43064097934658,-1.38981975448008,
-1.37050017754913,-1.35786409561476,-1.31261008774766,-1.28845427025889,
-1.27348742951611,-1.26735607988056,-1.22135965381363,-1.19019967921242,
-1.17501181051023,-1.16180282365541,-1.11361404212322,-1.08537774561768,
-1.065681746774,-1.01734234602368,-1.01298361676717,-0.989800484743978,
-0.975660060478834,-0.961400646454977,-0.91297299496954,-0.877560687902226,
-0.863256112850122,-0.813467002274696,-0.778613792962482,-0.758765854754386,
-0.748771882229555,-0.699694013065078,-0.665063849425104,-0.652432853856956,
-0.601574466772476,-0.567408266864309,-0.554246040117398,-0.503179057699677,
-0.47453584766665,-0.452597563304486,-0.438843075191766,-0.388240164207818,
-0.339992631709086,-0.324961067406404,-0.272319516847208,-0.244626537225397,
-0.228899959068603,-0.219677966288012),.UNSPECIFIED.);
#347=B_SPLINE_CURVE_WITH_KNOTS('',3,(#15912,#15913,#15914,#15915,#15916,
#15917,#15918,#15919,#15920,#15921,#15922,#15923,#15924,#15925,#15926,#15927,
#15928,#15929,#15930,#15931,#15932,#15933,#15934,#15935,#15936,#15937,#15938,
#15939,#15940,#15941,#15942,#15943,#15944,#15945,#15946,#15947,#15948,#15949,
#15950,#15951),.UNSPECIFIED.,.F.,.F.,(4,3,3,3,3,3,3,3,3,3,3,3,3,4),(-0.410648750432942,
-0.358826089191368,-0.328029287072579,-0.308519004108926,-0.296262202932191,
-0.26150895880243,-0.216116614902301,-0.200333794334701,-0.187454170065865,
-0.140590627549399,-0.100700164313061,-0.0879171980596439,-0.0431115726344213,
0.),.UNSPECIFIED.);
#348=B_SPLINE_CURVE_WITH_KNOTS('',3,(#15954,#15955,#15956,#15957,#15958,
#15959,#15960,#15961,#15962,#15963,#15964,#15965,#15966,#15967,#15968,#15969,
#15970,#15971,#15972),.UNSPECIFIED.,.F.,.F.,(4,3,3,3,3,3,4),(-0.219677966288012,
-0.190520484895311,-0.142890363671484,-0.122211652786797,-0.104525518218166,
-0.051044179373176,0.),.UNSPECIFIED.);
#349=B_SPLINE_CURVE_WITH_KNOTS('',3,(#16181,#16182,#16183,#16184,#16185,
#16186,#16187,#16188),.UNSPECIFIED.,.F.,.F.,(4,1,1,1,1,4),(11.6150328478183,
12.6135684378078,13.6121040277972,14.6106396177866,15.609175207776,15.707963267949),
 .UNSPECIFIED.);
#350=B_SPLINE_CURVE_WITH_KNOTS('',3,(#16189,#16190,#16191,#16192,#16193,
#16194,#16195,#16196,#16197,#16198,#16199,#16200,#16201,#16202,#16203,#16204,
#16205,#16206,#16207,#16208,#16209,#16210,#16211,#16212,#16213,#16214,#16215,
#16216,#16217,#16218,#16219,#16220,#16221,#16222,#16223,#16224,#16225,#16226,
#16227,#16228,#16229,#16230,#16231,#16232,#16233,#16234,#16235,#16236,#16237,
#16238,#16239,#16240,#16241,#16242,#16243,#16244,#16245,#16246),
 .UNSPECIFIED.,.F.,.F.,(4,3,3,3,3,3,3,3,3,3,3,3,3,3,3,3,3,3,3,4),(-0.552745378375022,
-0.531732216109367,-0.495433585222867,-0.478320891961644,-0.462732594796475,
-0.411092485600477,-0.390677853577304,-0.340757312661949,-0.30860231212099,
-0.294836984398962,-0.28154793240529,-0.252586719916514,-0.203516171016912,
-0.190166931037024,-0.142625198277768,-0.106027264752,-0.0927756455088851,
-0.0463878227544426,-0.0029163339731809,0.),.UNSPECIFIED.);
#351=B_SPLINE_CURVE_WITH_KNOTS('',3,(#16247,#16248,#16249,#16250,#16251,
#16252,#16253,#16254,#16255,#16256,#16257,#16258,#16259,#16260,#16261,#16262,
#16263,#16264,#16265),.UNSPECIFIED.,.F.,.F.,(4,3,3,3,3,3,4),(-46.4153600729827,
-45.9326371395139,-44.9341015495244,-43.935565959535,-42.9370303695455,
-41.9384947795561,-41.7920422632081),.UNSPECIFIED.);
#352=B_SPLINE_CURVE_WITH_KNOTS('',3,(#16268,#16269,#16270,#16271,#16272,
#16273,#16274,#16275,#16276),.UNSPECIFIED.,.F.,.F.,(4,1,1,1,1,1,4),(10.3761157273101,
11.3073783420651,12.3073452719531,13.3073122018412,14.3072791317292,15.3072460616173,
15.707963267949),.UNSPECIFIED.);
#353=B_SPLINE_CURVE_WITH_KNOTS('',3,(#16490,#16491,#16492,#16493,#16494,
#16495,#16496,#16497,#16498,#16499,#16500,#16501,#16502,#16503,#16504,#16505,
#16506,#16507,#16508,#16509,#16510,#16511),.UNSPECIFIED.,.F.,.F.,(4,3,3,
3,3,3,3,4),(38.8164122514459,38.9987102656334,39.9986771955214,40.9986441254095,
41.9986110552975,42.9985779851855,43.9985449150736,44.3467218980736),
 .UNSPECIFIED.);
#354=B_SPLINE_CURVE_WITH_KNOTS('',3,(#16512,#16513,#16514,#16515,#16516,
#16517,#16518,#16519,#16520,#16521,#16522,#16523,#16524,#16525,#16526,#16527,
#16528,#16529,#16530,#16531,#16532,#16533,#16534,#16535,#16536,#16537,#16538,
#16539,#16540,#16541,#16542,#16543,#16544,#16545,#16546,#16547,#16548,#16549,
#16550,#16551,#16552,#16553,#16554,#16555,#16556,#16557,#16558,#16559,#16560,
#16561,#16562,#16563,#16564,#16565,#16566),.UNSPECIFIED.,.F.,.F.,(4,3,3,
3,3,3,3,3,3,3,3,3,3,3,3,3,3,3,4),(-0.555272788399379,-0.538723215789889,
-0.502505759606931,-0.480336511409691,-0.450262499357502,-0.432260064517123,
-0.415086800376396,-0.367002820174333,-0.33403854157658,-0.315897619343378,
-0.282970454249822,-0.247599147468594,-0.225194500794938,-0.211702649714103,
-0.16177555555491,-0.11641698228548,-0.102903245473459,-0.0505012129231342,
0.),.UNSPECIFIED.);
#373=SHAPE_REPRESENTATION_RELATIONSHIP('SRR','None',#16782,#392);
#392=ADVANCED_BREP_SHAPE_REPRESENTATION('',(#430),#16686);
#411=STYLED_ITEM('',(#16881),#430);
#430=MANIFOLD_SOLID_BREP('Body1',#6130);
#551=FACE_BOUND('',#1497,.T.);
#552=FACE_BOUND('',#1500,.T.);
#675=PLANE('',#6942);
#676=PLANE('',#6944);
#677=PLANE('',#6945);
#678=PLANE('',#6946);
#679=PLANE('',#6947);
#680=PLANE('',#6948);
#681=PLANE('',#6949);
#682=PLANE('',#6950);
#683=PLANE('',#6951);
#684=PLANE('',#6955);
#685=PLANE('',#6956);
#1002=FACE_OUTER_BOUND('',#1469,.T.);
#1003=FACE_OUTER_BOUND('',#1470,.T.);
#1004=FACE_OUTER_BOUND('',#1471,.T.);
#1005=FACE_OUTER_BOUND('',#1472,.T.);
#1006=FACE_OUTER_BOUND('',#1473,.T.);
#1007=FACE_OUTER_BOUND('',#1474,.T.);
#1008=FACE_OUTER_BOUND('',#1475,.T.);
#1009=FACE_OUTER_BOUND('',#1476,.T.);
#1010=FACE_OUTER_BOUND('',#1477,.T.);
#1011=FACE_OUTER_BOUND('',#1478,.T.);
#1012=FACE_OUTER_BOUND('',#1479,.T.);
#1013=FACE_OUTER_BOUND('',#1480,.T.);
#1014=FACE_OUTER_BOUND('',#1481,.T.);
#1015=FACE_OUTER_BOUND('',#1482,.T.);
#1016=FACE_OUTER_BOUND('',#1483,.T.);
#1017=FACE_OUTER_BOUND('',#1484,.T.);
#1018=FACE_OUTER_BOUND('',#1485,.T.);
#1019=FACE_OUTER_BOUND('',#1486,.T.);
#1020=FACE_OUTER_BOUND('',#1487,.T.);
#1021=FACE_OUTER_BOUND('',#1488,.T.);
#1022=FACE_OUTER_BOUND('',#1489,.T.);
#1023=FACE_OUTER_BOUND('',#1490,.T.);
#1024=FACE_OUTER_BOUND('',#1491,.T.);
#1025=FACE_OUTER_BOUND('',#1492,.T.);
#1026=FACE_OUTER_BOUND('',#1493,.T.);
#1027=FACE_OUTER_BOUND('',#1494,.T.);
#1028=FACE_OUTER_BOUND('',#1495,.T.);
#1029=FACE_OUTER_BOUND('',#1496,.T.);
#1030=FACE_OUTER_BOUND('',#1498,.T.);
#1031=FACE_OUTER_BOUND('',#1499,.T.);
#1032=FACE_OUTER_BOUND('',#1501,.T.);
#1469=EDGE_LOOP('',(#5401,#5402,#5403,#5404,#5405,#5406,#5407,#5408));
#1470=EDGE_LOOP('',(#5409,#5410,#5411,#5412));
#1471=EDGE_LOOP('',(#5413,#5414,#5415,#5416));
#1472=EDGE_LOOP('',(#5417,#5418,#5419,#5420));
#1473=EDGE_LOOP('',(#5421,#5422,#5423,#5424));
#1474=EDGE_LOOP('',(#5425,#5426,#5427,#5428));
#1475=EDGE_LOOP('',(#5429,#5430,#5431,#5432));
#1476=EDGE_LOOP('',(#5433,#5434,#5435,#5436));
#1477=EDGE_LOOP('',(#5437,#5438,#5439,#5440));
#1478=EDGE_LOOP('',(#5441,#5442,#5443,#5444));
#1479=EDGE_LOOP('',(#5445,#5446,#5447,#5448));
#1480=EDGE_LOOP('',(#5449,#5450,#5451,#5452));
#1481=EDGE_LOOP('',(#5453,#5454,#5455,#5456));
#1482=EDGE_LOOP('',(#5457,#5458,#5459,#5460));
#1483=EDGE_LOOP('',(#5461,#5462,#5463,#5464,#5465,#5466,#5467,#5468));
#1484=EDGE_LOOP('',(#5469,#5470,#5471,#5472,#5473,#5474,#5475,#5476,#5477,
#5478,#5479,#5480,#5481,#5482,#5483,#5484,#5485,#5486));
#1485=EDGE_LOOP('',(#5487,#5488,#5489,#5490));
#1486=EDGE_LOOP('',(#5491,#5492,#5493,#5494,#5495,#5496,#5497,#5498,#5499,
#5500,#5501,#5502,#5503,#5504,#5505,#5506,#5507,#5508,#5509));
#1487=EDGE_LOOP('',(#5510,#5511,#5512,#5513,#5514));
#1488=EDGE_LOOP('',(#5515,#5516,#5517,#5518));
#1489=EDGE_LOOP('',(#5519,#5520,#5521,#5522));
#1490=EDGE_LOOP('',(#5523,#5524,#5525,#5526));
#1491=EDGE_LOOP('',(#5527,#5528,#5529,#5530));
#1492=EDGE_LOOP('',(#5531,#5532,#5533,#5534));
#1493=EDGE_LOOP('',(#5535,#5536,#5537,#5538));
#1494=EDGE_LOOP('',(#5539,#5540,#5541,#5542));
#1495=EDGE_LOOP('',(#5543,#5544,#5545,#5546,#5547,#5548));
#1496=EDGE_LOOP('',(#5549));
#1497=EDGE_LOOP('',(#5550));
#1498=EDGE_LOOP('',(#5551,#5552,#5553,#5554));
#1499=EDGE_LOOP('',(#5555));
#1500=EDGE_LOOP('',(#5556,#5557,#5558,#5559,#5560,#5561));
#1501=EDGE_LOOP('',(#5562));
#1836=LINE('',#15278,#2205);
#1837=LINE('',#15293,#2206);
#1838=LINE('',#15307,#2207);
#1839=LINE('',#15355,#2208);
#1840=LINE('',#15403,#2209);
#1841=LINE('',#15451,#2210);
#1842=LINE('',#15505,#2211);
#1843=LINE('',#15553,#2212);
#1844=LINE('',#15601,#2213);
#1845=LINE('',#15626,#2214);
#1846=LINE('',#15651,#2215);
#1847=LINE('',#15675,#2216);
#1848=LINE('',#15700,#2217);
#1849=LINE('',#15725,#2218);
#1850=LINE('',#15749,#2219);
#1851=LINE('',#15974,#2220);
#1852=LINE('',#16572,#2221);
#1853=LINE('',#16574,#2222);
#1854=LINE('',#16576,#2223);
#1855=LINE('',#16577,#2224);
#1856=LINE('',#16580,#2225);
#1857=LINE('',#16582,#2226);
#1858=LINE('',#16583,#2227);
#1859=LINE('',#16586,#2228);
#1860=LINE('',#16588,#2229);
#1861=LINE('',#16589,#2230);
#1862=LINE('',#16592,#2231);
#1863=LINE('',#16594,#2232);
#1864=LINE('',#16595,#2233);
#1865=LINE('',#16598,#2234);
#1866=LINE('',#16600,#2235);
#1867=LINE('',#16601,#2236);
#1868=LINE('',#16603,#2237);
#1869=LINE('',#16604,#2238);
#1870=LINE('',#16611,#2239);
#2205=VECTOR('',#8480,0.3);
#2206=VECTOR('',#8483,0.3);
#2207=VECTOR('',#8490,0.3);
#2208=VECTOR('',#8493,0.3);
#2209=VECTOR('',#8496,0.3);
#2210=VECTOR('',#8499,0.3);
#2211=VECTOR('',#8502,0.3);
#2212=VECTOR('',#8505,0.3);
#2213=VECTOR('',#8508,0.237175);
#2214=VECTOR('',#8513,0.237175);
#2215=VECTOR('',#8516,0.237175);
#2216=VECTOR('',#8519,0.237175);
#2217=VECTOR('',#8522,0.237175);
#2218=VECTOR('',#8525,0.237175);
#2219=VECTOR('',#8528,0.237175);
#2220=VECTOR('',#8533,0.25);
#2221=VECTOR('',#8546,1.);
#2222=VECTOR('',#8547,1.);
#2223=VECTOR('',#8548,1.);
#2224=VECTOR('',#8549,1.);
#2225=VECTOR('',#8552,1.);
#2226=VECTOR('',#8553,1.);
#2227=VECTOR('',#8554,1.);
#2228=VECTOR('',#8557,1.);
#2229=VECTOR('',#8558,1.);
#2230=VECTOR('',#8559,1.);
#2231=VECTOR('',#8562,1.);
#2232=VECTOR('',#8563,1.);
#2233=VECTOR('',#8564,1.);
#2234=VECTOR('',#8567,1.);
#2235=VECTOR('',#8568,1.);
#2236=VECTOR('',#8569,1.);
#2237=VECTOR('',#8572,1.);
#2238=VECTOR('',#8573,1.);
#2239=VECTOR('',#8582,0.5);
#2490=CIRCLE('',#6920,0.2942);
#2491=CIRCLE('',#6921,0.2942);
#2492=CIRCLE('',#6922,0.2942);
#2493=CIRCLE('',#6930,0.237175);
#2494=CIRCLE('',#6938,0.2942);
#2495=CIRCLE('',#6939,0.199999999999999);
#2496=CIRCLE('',#6941,0.237175);
#2497=CIRCLE('',#6952,0.5);
#2498=CIRCLE('',#6954,0.5);
#3001=VERTEX_POINT('',#15276);
#3002=VERTEX_POINT('',#15277);
#3003=VERTEX_POINT('',#15279);
#3004=VERTEX_POINT('',#15290);
#3005=VERTEX_POINT('',#15292);
#3006=VERTEX_POINT('',#15295);
#3007=VERTEX_POINT('',#15305);
#3008=VERTEX_POINT('',#15306);
#3009=VERTEX_POINT('',#15353);
#3010=VERTEX_POINT('',#15354);
#3011=VERTEX_POINT('',#15401);
#3012=VERTEX_POINT('',#15402);
#3013=VERTEX_POINT('',#15449);
#3014=VERTEX_POINT('',#15450);
#3015=VERTEX_POINT('',#15503);
#3016=VERTEX_POINT('',#15504);
#3017=VERTEX_POINT('',#15551);
#3018=VERTEX_POINT('',#15552);
#3019=VERTEX_POINT('',#15599);
#3020=VERTEX_POINT('',#15600);
#3021=VERTEX_POINT('',#15602);
#3022=VERTEX_POINT('',#15613);
#3023=VERTEX_POINT('',#15624);
#3024=VERTEX_POINT('',#15625);
#3025=VERTEX_POINT('',#15649);
#3026=VERTEX_POINT('',#15650);
#3027=VERTEX_POINT('',#15673);
#3028=VERTEX_POINT('',#15674);
#3029=VERTEX_POINT('',#15698);
#3030=VERTEX_POINT('',#15699);
#3031=VERTEX_POINT('',#15723);
#3032=VERTEX_POINT('',#15724);
#3033=VERTEX_POINT('',#15747);
#3034=VERTEX_POINT('',#15748);
#3035=VERTEX_POINT('',#15771);
#3036=VERTEX_POINT('',#15911);
#3037=VERTEX_POINT('',#15952);
#3038=VERTEX_POINT('',#15973);
#3039=VERTEX_POINT('',#16180);
#3040=VERTEX_POINT('',#16267);
#3041=VERTEX_POINT('',#16570);
#3042=VERTEX_POINT('',#16571);
#3043=VERTEX_POINT('',#16573);
#3044=VERTEX_POINT('',#16575);
#3045=VERTEX_POINT('',#16579);
#3046=VERTEX_POINT('',#16581);
#3047=VERTEX_POINT('',#16585);
#3048=VERTEX_POINT('',#16587);
#3049=VERTEX_POINT('',#16591);
#3050=VERTEX_POINT('',#16593);
#3051=VERTEX_POINT('',#16597);
#3052=VERTEX_POINT('',#16599);
#3053=VERTEX_POINT('',#16607);
#3054=VERTEX_POINT('',#16610);
#3810=EDGE_CURVE('',#3001,#3002,#1836,.T.);
#3811=EDGE_CURVE('',#3001,#3003,#318,.T.);
#3812=EDGE_CURVE('',#3003,#3004,#2490,.T.);
#3813=EDGE_CURVE('',#3004,#3005,#1837,.T.);
#3814=EDGE_CURVE('',#3005,#3005,#2491,.F.);
#3815=EDGE_CURVE('',#3004,#3006,#2492,.T.);
#3816=EDGE_CURVE('',#3006,#3002,#319,.T.);
#3817=EDGE_CURVE('',#3007,#3008,#1838,.T.);
#3818=EDGE_CURVE('',#3007,#3001,#320,.T.);
#3819=EDGE_CURVE('',#3002,#3008,#321,.T.);
#3820=EDGE_CURVE('',#3009,#3010,#1839,.T.);
#3821=EDGE_CURVE('',#3009,#3007,#322,.T.);
#3822=EDGE_CURVE('',#3008,#3010,#323,.T.);
#3823=EDGE_CURVE('',#3011,#3012,#1840,.T.);
#3824=EDGE_CURVE('',#3011,#3009,#324,.T.);
#3825=EDGE_CURVE('',#3010,#3012,#325,.T.);
#3826=EDGE_CURVE('',#3013,#3014,#1841,.T.);
#3827=EDGE_CURVE('',#3013,#3011,#326,.T.);
#3828=EDGE_CURVE('',#3012,#3014,#327,.T.);
#3829=EDGE_CURVE('',#3015,#3016,#1842,.T.);
#3830=EDGE_CURVE('',#3015,#3013,#328,.T.);
#3831=EDGE_CURVE('',#3014,#3016,#329,.T.);
#3832=EDGE_CURVE('',#3017,#3018,#1843,.T.);
#3833=EDGE_CURVE('',#3017,#3015,#330,.T.);
#3834=EDGE_CURVE('',#3016,#3018,#331,.T.);
#3835=EDGE_CURVE('',#3019,#3020,#1844,.T.);
#3836=EDGE_CURVE('',#3019,#3021,#332,.T.);
#3837=EDGE_CURVE('',#3021,#3022,#2493,.T.);
#3838=EDGE_CURVE('',#3020,#3022,#333,.T.);
#3839=EDGE_CURVE('',#3023,#3024,#1845,.T.);
#3840=EDGE_CURVE('',#3023,#3019,#334,.T.);
#3841=EDGE_CURVE('',#3024,#3020,#335,.T.);
#3842=EDGE_CURVE('',#3025,#3026,#1846,.T.);
#3843=EDGE_CURVE('',#3025,#3023,#336,.T.);
#3844=EDGE_CURVE('',#3026,#3024,#337,.T.);
#3845=EDGE_CURVE('',#3027,#3028,#1847,.T.);
#3846=EDGE_CURVE('',#3027,#3025,#338,.T.);
#3847=EDGE_CURVE('',#3028,#3026,#339,.T.);
#3848=EDGE_CURVE('',#3029,#3030,#1848,.T.);
#3849=EDGE_CURVE('',#3029,#3027,#340,.T.);
#3850=EDGE_CURVE('',#3030,#3028,#341,.T.);
#3851=EDGE_CURVE('',#3031,#3032,#1849,.T.);
#3852=EDGE_CURVE('',#3031,#3029,#342,.T.);
#3853=EDGE_CURVE('',#3032,#3030,#343,.T.);
#3854=EDGE_CURVE('',#3033,#3034,#1850,.T.);
#3855=EDGE_CURVE('',#3033,#3031,#344,.T.);
#3856=EDGE_CURVE('',#3034,#3032,#345,.T.);
#3857=EDGE_CURVE('',#3022,#3035,#346,.T.);
#3858=EDGE_CURVE('',#3036,#3021,#347,.T.);
#3859=EDGE_CURVE('',#3037,#3036,#2494,.T.);
#3860=EDGE_CURVE('',#3035,#3037,#348,.T.);
#3861=EDGE_CURVE('',#3035,#3038,#1851,.T.);
#3862=EDGE_CURVE('',#3038,#3038,#2495,.T.);
#3863=EDGE_CURVE('',#3039,#3033,#349,.T.);
#3864=EDGE_CURVE('',#3003,#3039,#350,.T.);
#3865=EDGE_CURVE('',#3036,#3017,#351,.T.);
#3866=EDGE_CURVE('',#3040,#3034,#352,.T.);
#3867=EDGE_CURVE('',#3039,#3040,#2496,.T.);
#3868=EDGE_CURVE('',#3018,#3037,#353,.T.);
#3869=EDGE_CURVE('',#3040,#3006,#354,.T.);
#3870=EDGE_CURVE('',#3041,#3042,#1852,.T.);
#3871=EDGE_CURVE('',#3041,#3043,#1853,.T.);
#3872=EDGE_CURVE('',#3043,#3044,#1854,.T.);
#3873=EDGE_CURVE('',#3042,#3044,#1855,.T.);
#3874=EDGE_CURVE('',#3045,#3041,#1856,.T.);
#3875=EDGE_CURVE('',#3045,#3046,#1857,.T.);
#3876=EDGE_CURVE('',#3046,#3043,#1858,.T.);
#3877=EDGE_CURVE('',#3047,#3045,#1859,.T.);
#3878=EDGE_CURVE('',#3047,#3048,#1860,.T.);
#3879=EDGE_CURVE('',#3048,#3046,#1861,.T.);
#3880=EDGE_CURVE('',#3049,#3047,#1862,.T.);
#3881=EDGE_CURVE('',#3049,#3050,#1863,.T.);
#3882=EDGE_CURVE('',#3050,#3048,#1864,.T.);
#3883=EDGE_CURVE('',#3051,#3049,#1865,.T.);
#3884=EDGE_CURVE('',#3051,#3052,#1866,.T.);
#3885=EDGE_CURVE('',#3052,#3050,#1867,.T.);
#3886=EDGE_CURVE('',#3042,#3051,#1868,.T.);
#3887=EDGE_CURVE('',#3044,#3052,#1869,.T.);
#3888=EDGE_CURVE('',#3053,#3053,#2497,.T.);
#3889=EDGE_CURVE('',#3053,#3054,#1870,.T.);
#3890=EDGE_CURVE('',#3054,#3054,#2498,.T.);
#5401=ORIENTED_EDGE('',*,*,#3810,.F.);
#5402=ORIENTED_EDGE('',*,*,#3811,.T.);
#5403=ORIENTED_EDGE('',*,*,#3812,.T.);
#5404=ORIENTED_EDGE('',*,*,#3813,.T.);
#5405=ORIENTED_EDGE('',*,*,#3814,.T.);
#5406=ORIENTED_EDGE('',*,*,#3813,.F.);
#5407=ORIENTED_EDGE('',*,*,#3815,.T.);
#5408=ORIENTED_EDGE('',*,*,#3816,.T.);
#5409=ORIENTED_EDGE('',*,*,#3817,.F.);
#5410=ORIENTED_EDGE('',*,*,#3818,.T.);
#5411=ORIENTED_EDGE('',*,*,#3810,.T.);
#5412=ORIENTED_EDGE('',*,*,#3819,.T.);
#5413=ORIENTED_EDGE('',*,*,#3820,.F.);
#5414=ORIENTED_EDGE('',*,*,#3821,.T.);
#5415=ORIENTED_EDGE('',*,*,#3817,.T.);
#5416=ORIENTED_EDGE('',*,*,#3822,.T.);
#5417=ORIENTED_EDGE('',*,*,#3823,.F.);
#5418=ORIENTED_EDGE('',*,*,#3824,.T.);
#5419=ORIENTED_EDGE('',*,*,#3820,.T.);
#5420=ORIENTED_EDGE('',*,*,#3825,.T.);
#5421=ORIENTED_EDGE('',*,*,#3826,.F.);
#5422=ORIENTED_EDGE('',*,*,#3827,.T.);
#5423=ORIENTED_EDGE('',*,*,#3823,.T.);
#5424=ORIENTED_EDGE('',*,*,#3828,.T.);
#5425=ORIENTED_EDGE('',*,*,#3829,.F.);
#5426=ORIENTED_EDGE('',*,*,#3830,.T.);
#5427=ORIENTED_EDGE('',*,*,#3826,.T.);
#5428=ORIENTED_EDGE('',*,*,#3831,.T.);
#5429=ORIENTED_EDGE('',*,*,#3832,.F.);
#5430=ORIENTED_EDGE('',*,*,#3833,.T.);
#5431=ORIENTED_EDGE('',*,*,#3829,.T.);
#5432=ORIENTED_EDGE('',*,*,#3834,.T.);
#5433=ORIENTED_EDGE('',*,*,#3835,.F.);
#5434=ORIENTED_EDGE('',*,*,#3836,.T.);
#5435=ORIENTED_EDGE('',*,*,#3837,.T.);
#5436=ORIENTED_EDGE('',*,*,#3838,.F.);
#5437=ORIENTED_EDGE('',*,*,#3839,.F.);
#5438=ORIENTED_EDGE('',*,*,#3840,.T.);
#5439=ORIENTED_EDGE('',*,*,#3835,.T.);
#5440=ORIENTED_EDGE('',*,*,#3841,.F.);
#5441=ORIENTED_EDGE('',*,*,#3842,.F.);
#5442=ORIENTED_EDGE('',*,*,#3843,.T.);
#5443=ORIENTED_EDGE('',*,*,#3839,.T.);
#5444=ORIENTED_EDGE('',*,*,#3844,.F.);
#5445=ORIENTED_EDGE('',*,*,#3845,.F.);
#5446=ORIENTED_EDGE('',*,*,#3846,.T.);
#5447=ORIENTED_EDGE('',*,*,#3842,.T.);
#5448=ORIENTED_EDGE('',*,*,#3847,.F.);
#5449=ORIENTED_EDGE('',*,*,#3848,.F.);
#5450=ORIENTED_EDGE('',*,*,#3849,.T.);
#5451=ORIENTED_EDGE('',*,*,#3845,.T.);
#5452=ORIENTED_EDGE('',*,*,#3850,.F.);
#5453=ORIENTED_EDGE('',*,*,#3851,.F.);
#5454=ORIENTED_EDGE('',*,*,#3852,.T.);
#5455=ORIENTED_EDGE('',*,*,#3848,.T.);
#5456=ORIENTED_EDGE('',*,*,#3853,.F.);
#5457=ORIENTED_EDGE('',*,*,#3854,.F.);
#5458=ORIENTED_EDGE('',*,*,#3855,.T.);
#5459=ORIENTED_EDGE('',*,*,#3851,.T.);
#5460=ORIENTED_EDGE('',*,*,#3856,.F.);
#5461=ORIENTED_EDGE('',*,*,#3857,.F.);
#5462=ORIENTED_EDGE('',*,*,#3837,.F.);
#5463=ORIENTED_EDGE('',*,*,#3858,.F.);
#5464=ORIENTED_EDGE('',*,*,#3859,.F.);
#5465=ORIENTED_EDGE('',*,*,#3860,.F.);
#5466=ORIENTED_EDGE('',*,*,#3861,.T.);
#5467=ORIENTED_EDGE('',*,*,#3862,.F.);
#5468=ORIENTED_EDGE('',*,*,#3861,.F.);
#5469=ORIENTED_EDGE('',*,*,#3858,.T.);
#5470=ORIENTED_EDGE('',*,*,#3836,.F.);
#5471=ORIENTED_EDGE('',*,*,#3840,.F.);
#5472=ORIENTED_EDGE('',*,*,#3843,.F.);
#5473=ORIENTED_EDGE('',*,*,#3846,.F.);
#5474=ORIENTED_EDGE('',*,*,#3849,.F.);
#5475=ORIENTED_EDGE('',*,*,#3852,.F.);
#5476=ORIENTED_EDGE('',*,*,#3855,.F.);
#5477=ORIENTED_EDGE('',*,*,#3863,.F.);
#5478=ORIENTED_EDGE('',*,*,#3864,.F.);
#5479=ORIENTED_EDGE('',*,*,#3811,.F.);
#5480=ORIENTED_EDGE('',*,*,#3818,.F.);
#5481=ORIENTED_EDGE('',*,*,#3821,.F.);
#5482=ORIENTED_EDGE('',*,*,#3824,.F.);
#5483=ORIENTED_EDGE('',*,*,#3827,.F.);
#5484=ORIENTED_EDGE('',*,*,#3830,.F.);
#5485=ORIENTED_EDGE('',*,*,#3833,.F.);
#5486=ORIENTED_EDGE('',*,*,#3865,.F.);
#5487=ORIENTED_EDGE('',*,*,#3854,.T.);
#5488=ORIENTED_EDGE('',*,*,#3866,.F.);
#5489=ORIENTED_EDGE('',*,*,#3867,.F.);
#5490=ORIENTED_EDGE('',*,*,#3863,.T.);
#5491=ORIENTED_EDGE('',*,*,#3857,.T.);
#5492=ORIENTED_EDGE('',*,*,#3860,.T.);
#5493=ORIENTED_EDGE('',*,*,#3868,.F.);
#5494=ORIENTED_EDGE('',*,*,#3834,.F.);
#5495=ORIENTED_EDGE('',*,*,#3831,.F.);
#5496=ORIENTED_EDGE('',*,*,#3828,.F.);
#5497=ORIENTED_EDGE('',*,*,#3825,.F.);
#5498=ORIENTED_EDGE('',*,*,#3822,.F.);
#5499=ORIENTED_EDGE('',*,*,#3819,.F.);
#5500=ORIENTED_EDGE('',*,*,#3816,.F.);
#5501=ORIENTED_EDGE('',*,*,#3869,.F.);
#5502=ORIENTED_EDGE('',*,*,#3866,.T.);
#5503=ORIENTED_EDGE('',*,*,#3856,.T.);
#5504=ORIENTED_EDGE('',*,*,#3853,.T.);
#5505=ORIENTED_EDGE('',*,*,#3850,.T.);
#5506=ORIENTED_EDGE('',*,*,#3847,.T.);
#5507=ORIENTED_EDGE('',*,*,#3844,.T.);
#5508=ORIENTED_EDGE('',*,*,#3841,.T.);
#5509=ORIENTED_EDGE('',*,*,#3838,.T.);
#5510=ORIENTED_EDGE('',*,*,#3812,.F.);
#5511=ORIENTED_EDGE('',*,*,#3864,.T.);
#5512=ORIENTED_EDGE('',*,*,#3867,.T.);
#5513=ORIENTED_EDGE('',*,*,#3869,.T.);
#5514=ORIENTED_EDGE('',*,*,#3815,.F.);
#5515=ORIENTED_EDGE('',*,*,#3832,.T.);
#5516=ORIENTED_EDGE('',*,*,#3868,.T.);
#5517=ORIENTED_EDGE('',*,*,#3859,.T.);
#5518=ORIENTED_EDGE('',*,*,#3865,.T.);
#5519=ORIENTED_EDGE('',*,*,#3870,.F.);
#5520=ORIENTED_EDGE('',*,*,#3871,.T.);
#5521=ORIENTED_EDGE('',*,*,#3872,.T.);
#5522=ORIENTED_EDGE('',*,*,#3873,.F.);
#5523=ORIENTED_EDGE('',*,*,#3874,.F.);
#5524=ORIENTED_EDGE('',*,*,#3875,.T.);
#5525=ORIENTED_EDGE('',*,*,#3876,.T.);
#5526=ORIENTED_EDGE('',*,*,#3871,.F.);
#5527=ORIENTED_EDGE('',*,*,#3877,.F.);
#5528=ORIENTED_EDGE('',*,*,#3878,.T.);
#5529=ORIENTED_EDGE('',*,*,#3879,.T.);
#5530=ORIENTED_EDGE('',*,*,#3875,.F.);
#5531=ORIENTED_EDGE('',*,*,#3880,.F.);
#5532=ORIENTED_EDGE('',*,*,#3881,.T.);
#5533=ORIENTED_EDGE('',*,*,#3882,.T.);
#5534=ORIENTED_EDGE('',*,*,#3878,.F.);
#5535=ORIENTED_EDGE('',*,*,#3883,.F.);
#5536=ORIENTED_EDGE('',*,*,#3884,.T.);
#5537=ORIENTED_EDGE('',*,*,#3885,.T.);
#5538=ORIENTED_EDGE('',*,*,#3881,.F.);
#5539=ORIENTED_EDGE('',*,*,#3886,.F.);
#5540=ORIENTED_EDGE('',*,*,#3873,.T.);
#5541=ORIENTED_EDGE('',*,*,#3887,.T.);
#5542=ORIENTED_EDGE('',*,*,#3884,.F.);
#5543=ORIENTED_EDGE('',*,*,#3887,.F.);
#5544=ORIENTED_EDGE('',*,*,#3872,.F.);
#5545=ORIENTED_EDGE('',*,*,#3876,.F.);
#5546=ORIENTED_EDGE('',*,*,#3879,.F.);
#5547=ORIENTED_EDGE('',*,*,#3882,.F.);
#5548=ORIENTED_EDGE('',*,*,#3885,.F.);
#5549=ORIENTED_EDGE('',*,*,#3888,.T.);
#5550=ORIENTED_EDGE('',*,*,#3814,.F.);
#5551=ORIENTED_EDGE('',*,*,#3888,.F.);
#5552=ORIENTED_EDGE('',*,*,#3889,.T.);
#5553=ORIENTED_EDGE('',*,*,#3890,.T.);
#5554=ORIENTED_EDGE('',*,*,#3889,.F.);
#5555=ORIENTED_EDGE('',*,*,#3890,.F.);
#5556=ORIENTED_EDGE('',*,*,#3870,.T.);
#5557=ORIENTED_EDGE('',*,*,#3886,.T.);
#5558=ORIENTED_EDGE('',*,*,#3883,.T.);
#5559=ORIENTED_EDGE('',*,*,#3880,.T.);
#5560=ORIENTED_EDGE('',*,*,#3877,.T.);
#5561=ORIENTED_EDGE('',*,*,#3874,.T.);
#5562=ORIENTED_EDGE('',*,*,#3862,.T.);
#5748=CYLINDRICAL_SURFACE('',#6919,0.2942);
#5749=CYLINDRICAL_SURFACE('',#6923,0.2942);
#5750=CYLINDRICAL_SURFACE('',#6924,0.2942);
#5751=CYLINDRICAL_SURFACE('',#6925,0.2942);
#5752=CYLINDRICAL_SURFACE('',#6926,0.2942);
#5753=CYLINDRICAL_SURFACE('',#6927,0.2942);
#5754=CYLINDRICAL_SURFACE('',#6928,0.2942);
#5755=CYLINDRICAL_SURFACE('',#6929,0.237175);
#5756=CYLINDRICAL_SURFACE('',#6931,0.237175);
#5757=CYLINDRICAL_SURFACE('',#6932,0.237175);
#5758=CYLINDRICAL_SURFACE('',#6933,0.237175);
#5759=CYLINDRICAL_SURFACE('',#6934,0.237175);
#5760=CYLINDRICAL_SURFACE('',#6935,0.237175);
#5761=CYLINDRICAL_SURFACE('',#6936,0.237175);
#5762=CYLINDRICAL_SURFACE('',#6940,0.237175);
#5763=CYLINDRICAL_SURFACE('',#6943,0.2942);
#5764=CYLINDRICAL_SURFACE('',#6953,0.5);
#6081=ADVANCED_FACE('',(#1002),#5748,.T.);
#6082=ADVANCED_FACE('',(#1003),#5749,.T.);
#6083=ADVANCED_FACE('',(#1004),#5750,.T.);
#6084=ADVANCED_FACE('',(#1005),#5751,.T.);
#6085=ADVANCED_FACE('',(#1006),#5752,.T.);
#6086=ADVANCED_FACE('',(#1007),#5753,.T.);
#6087=ADVANCED_FACE('',(#1008),#5754,.T.);
#6088=ADVANCED_FACE('',(#1009),#5755,.T.);
#6089=ADVANCED_FACE('',(#1010),#5756,.T.);
#6090=ADVANCED_FACE('',(#1011),#5757,.T.);
#6091=ADVANCED_FACE('',(#1012),#5758,.T.);
#6092=ADVANCED_FACE('',(#1013),#5759,.T.);
#6093=ADVANCED_FACE('',(#1014),#5760,.T.);
#6094=ADVANCED_FACE('',(#1015),#5761,.T.);
#6095=ADVANCED_FACE('',(#1016),#135,.T.);
#6096=ADVANCED_FACE('',(#1017),#146,.F.);
#6097=ADVANCED_FACE('',(#1018),#5762,.T.);
#6098=ADVANCED_FACE('',(#1019),#147,.F.);
#6099=ADVANCED_FACE('',(#1020),#675,.T.);
#6100=ADVANCED_FACE('',(#1021),#5763,.T.);
#6101=ADVANCED_FACE('',(#1022),#676,.F.);
#6102=ADVANCED_FACE('',(#1023),#677,.F.);
#6103=ADVANCED_FACE('',(#1024),#678,.F.);
#6104=ADVANCED_FACE('',(#1025),#679,.F.);
#6105=ADVANCED_FACE('',(#1026),#680,.F.);
#6106=ADVANCED_FACE('',(#1027),#681,.F.);
#6107=ADVANCED_FACE('',(#1028),#682,.F.);
#6108=ADVANCED_FACE('',(#1029,#551),#683,.T.);
#6109=ADVANCED_FACE('',(#1030),#5764,.T.);
#6110=ADVANCED_FACE('',(#1031,#552),#684,.F.);
#6111=ADVANCED_FACE('',(#1032),#685,.T.);
#6130=CLOSED_SHELL('',(#6081,#6082,#6083,#6084,#6085,#6086,#6087,#6088,
#6089,#6090,#6091,#6092,#6093,#6094,#6095,#6096,#6097,#6098,#6099,#6100,
#6101,#6102,#6103,#6104,#6105,#6106,#6107,#6108,#6109,#6110,#6111));
#6918=AXIS2_PLACEMENT_3D('',#15274,#8476,#8477);
#6919=AXIS2_PLACEMENT_3D('',#15275,#8478,#8479);
#6920=AXIS2_PLACEMENT_3D('',#15291,#8481,#8482);
#6921=AXIS2_PLACEMENT_3D('',#15294,#8484,#8485);
#6922=AXIS2_PLACEMENT_3D('',#15296,#8486,#8487);
#6923=AXIS2_PLACEMENT_3D('',#15304,#8488,#8489);
#6924=AXIS2_PLACEMENT_3D('',#15352,#8491,#8492);
#6925=AXIS2_PLACEMENT_3D('',#15400,#8494,#8495);
#6926=AXIS2_PLACEMENT_3D('',#15448,#8497,#8498);
#6927=AXIS2_PLACEMENT_3D('',#15502,#8500,#8501);
#6928=AXIS2_PLACEMENT_3D('',#15550,#8503,#8504);
#6929=AXIS2_PLACEMENT_3D('',#15598,#8506,#8507);
#6930=AXIS2_PLACEMENT_3D('',#15614,#8509,#8510);
#6931=AXIS2_PLACEMENT_3D('',#15623,#8511,#8512);
#6932=AXIS2_PLACEMENT_3D('',#15648,#8514,#8515);
#6933=AXIS2_PLACEMENT_3D('',#15672,#8517,#8518);
#6934=AXIS2_PLACEMENT_3D('',#15697,#8520,#8521);
#6935=AXIS2_PLACEMENT_3D('',#15722,#8523,#8524);
#6936=AXIS2_PLACEMENT_3D('',#15746,#8526,#8527);
#6937=AXIS2_PLACEMENT_3D('',#15770,#8529,#8530);
#6938=AXIS2_PLACEMENT_3D('',#15953,#8531,#8532);
#6939=AXIS2_PLACEMENT_3D('',#15975,#8534,#8535);
#6940=AXIS2_PLACEMENT_3D('',#16266,#8536,#8537);
#6941=AXIS2_PLACEMENT_3D('',#16277,#8538,#8539);
#6942=AXIS2_PLACEMENT_3D('',#16567,#8540,#8541);
#6943=AXIS2_PLACEMENT_3D('',#16568,#8542,#8543);
#6944=AXIS2_PLACEMENT_3D('',#16569,#8544,#8545);
#6945=AXIS2_PLACEMENT_3D('',#16578,#8550,#8551);
#6946=AXIS2_PLACEMENT_3D('',#16584,#8555,#8556);
#6947=AXIS2_PLACEMENT_3D('',#16590,#8560,#8561);
#6948=AXIS2_PLACEMENT_3D('',#16596,#8565,#8566);
#6949=AXIS2_PLACEMENT_3D('',#16602,#8570,#8571);
#6950=AXIS2_PLACEMENT_3D('',#16605,#8574,#8575);
#6951=AXIS2_PLACEMENT_3D('',#16606,#8576,#8577);
#6952=AXIS2_PLACEMENT_3D('',#16608,#8578,#8579);
#6953=AXIS2_PLACEMENT_3D('',#16609,#8580,#8581);
#6954=AXIS2_PLACEMENT_3D('',#16612,#8583,#8584);
#6955=AXIS2_PLACEMENT_3D('',#16613,#8585,#8586);
#6956=AXIS2_PLACEMENT_3D('',#16614,#8587,#8588);
#8476=DIRECTION('axis',(0.,0.,1.));
#8477=DIRECTION('refdir',(1.,0.,0.));
#8478=DIRECTION('center_axis',(0.,0.,1.));
#8479=DIRECTION('ref_axis',(1.,0.,0.));
#8480=DIRECTION('',(0.,0.,-1.));
#8481=DIRECTION('center_axis',(0.,0.,-1.));
#8482=DIRECTION('ref_axis',(1.,0.,0.));
#8483=DIRECTION('',(0.,0.,-1.));
#8484=DIRECTION('center_axis',(0.,0.,-1.));
#8485=DIRECTION('ref_axis',(1.,0.,0.));
#8486=DIRECTION('center_axis',(0.,0.,-1.));
#8487=DIRECTION('ref_axis',(1.,0.,0.));
#8488=DIRECTION('center_axis',(0.,0.,1.));
#8489=DIRECTION('ref_axis',(1.,0.,0.));
#8490=DIRECTION('',(0.,0.,-1.));
#8491=DIRECTION('center_axis',(0.,0.,1.));
#8492=DIRECTION('ref_axis',(1.,0.,0.));
#8493=DIRECTION('',(0.,0.,-1.));
#8494=DIRECTION('center_axis',(0.,0.,1.));
#8495=DIRECTION('ref_axis',(1.,0.,0.));
#8496=DIRECTION('',(0.,0.,-1.));
#8497=DIRECTION('center_axis',(0.,0.,1.));
#8498=DIRECTION('ref_axis',(1.,0.,0.));
#8499=DIRECTION('',(0.,0.,-1.));
#8500=DIRECTION('center_axis',(0.,0.,1.));
#8501=DIRECTION('ref_axis',(1.,0.,0.));
#8502=DIRECTION('',(0.,0.,-1.));
#8503=DIRECTION('center_axis',(0.,0.,1.));
#8504=DIRECTION('ref_axis',(1.,0.,0.));
#8505=DIRECTION('',(0.,0.,-1.));
#8506=DIRECTION('center_axis',(0.,0.,1.));
#8507=DIRECTION('ref_axis',(0.99733299283639,-0.0729856246120375,0.));
#8508=DIRECTION('',(0.,0.,1.));
#8509=DIRECTION('center_axis',(0.,0.,-1.));
#8510=DIRECTION('ref_axis',(1.,4.21694431476393E-14,0.));
#8511=DIRECTION('center_axis',(0.,0.,1.));
#8512=DIRECTION('ref_axis',(1.,4.21694431476393E-14,0.));
#8513=DIRECTION('',(0.,0.,1.));
#8514=DIRECTION('center_axis',(0.,0.,1.));
#8515=DIRECTION('ref_axis',(1.,4.21694431476393E-14,0.));
#8516=DIRECTION('',(0.,0.,1.));
#8517=DIRECTION('center_axis',(0.,0.,1.));
#8518=DIRECTION('ref_axis',(1.,4.21694431476393E-14,0.));
#8519=DIRECTION('',(0.,0.,1.));
#8520=DIRECTION('center_axis',(0.,0.,1.));
#8521=DIRECTION('ref_axis',(1.,4.21694431476393E-14,0.));
#8522=DIRECTION('',(0.,0.,1.));
#8523=DIRECTION('center_axis',(0.,0.,1.));
#8524=DIRECTION('ref_axis',(1.,4.21694431476393E-14,0.));
#8525=DIRECTION('',(0.,0.,1.));
#8526=DIRECTION('center_axis',(0.,0.,1.));
#8527=DIRECTION('ref_axis',(1.,4.21694431476393E-14,0.));
#8528=DIRECTION('',(0.,0.,1.));
#8529=DIRECTION('center_axis',(0.,0.,-1.));
#8530=DIRECTION('ref_axis',(1.,0.,0.));
#8531=DIRECTION('center_axis',(0.,0.,-1.));
#8532=DIRECTION('ref_axis',(1.,0.,0.));
#8533=DIRECTION('',(0.707106781186549,8.65956056235495E-17,0.707106781186546));
#8534=DIRECTION('center_axis',(0.,0.,1.));
#8535=DIRECTION('ref_axis',(1.,0.,0.));
#8536=DIRECTION('center_axis',(0.,0.,1.));
#8537=DIRECTION('ref_axis',(1.,4.21694431476393E-14,0.));
#8538=DIRECTION('center_axis',(0.,0.,-1.));
#8539=DIRECTION('ref_axis',(1.,4.21694431476393E-14,0.));
#8540=DIRECTION('center_axis',(0.,0.,1.));
#8541=DIRECTION('ref_axis',(1.,0.,0.));
#8542=DIRECTION('center_axis',(0.,0.,1.));
#8543=DIRECTION('ref_axis',(1.,0.,0.));
#8544=DIRECTION('center_axis',(-1.92296268638356E-16,-1.,0.));
#8545=DIRECTION('ref_axis',(1.,-1.92296268638356E-16,0.));
#8546=DIRECTION('',(1.,-1.92296268638356E-16,0.));
#8547=DIRECTION('',(0.,0.,1.));
#8548=DIRECTION('',(1.,-1.92296268638356E-16,0.));
#8549=DIRECTION('',(0.,0.,1.));
#8550=DIRECTION('center_axis',(-0.866025403784439,-0.5,0.));
#8551=DIRECTION('ref_axis',(0.5,-0.866025403784439,0.));
#8552=DIRECTION('',(0.5,-0.866025403784439,0.));
#8553=DIRECTION('',(0.,0.,1.));
#8554=DIRECTION('',(0.5,-0.866025403784439,0.));
#8555=DIRECTION('center_axis',(-0.866025403784439,0.5,0.));
#8556=DIRECTION('ref_axis',(-0.5,-0.866025403784439,0.));
#8557=DIRECTION('',(-0.5,-0.866025403784439,0.));
#8558=DIRECTION('',(0.,0.,1.));
#8559=DIRECTION('',(-0.5,-0.866025403784438,0.));
#8560=DIRECTION('center_axis',(1.92296268638356E-16,1.,0.));
#8561=DIRECTION('ref_axis',(-1.,1.92296268638356E-16,0.));
#8562=DIRECTION('',(-1.,1.92296268638356E-16,0.));
#8563=DIRECTION('',(0.,0.,1.));
#8564=DIRECTION('',(-1.,1.92296268638356E-16,0.));
#8565=DIRECTION('center_axis',(0.866025403784439,0.5,0.));
#8566=DIRECTION('ref_axis',(-0.5,0.866025403784439,0.));
#8567=DIRECTION('',(-0.5,0.866025403784439,0.));
#8568=DIRECTION('',(0.,0.,1.));
#8569=DIRECTION('',(-0.5,0.866025403784439,0.));
#8570=DIRECTION('center_axis',(0.866025403784439,-0.5,0.));
#8571=DIRECTION('ref_axis',(0.5,0.866025403784439,0.));
#8572=DIRECTION('',(0.5,0.866025403784439,0.));
#8573=DIRECTION('',(0.5,0.866025403784439,0.));
#8574=DIRECTION('center_axis',(0.,0.,1.));
#8575=DIRECTION('ref_axis',(1.,0.,0.));
#8576=DIRECTION('center_axis',(0.,0.,1.));
#8577=DIRECTION('ref_axis',(1.,0.,0.));
#8578=DIRECTION('center_axis',(0.,0.,1.));
#8579=DIRECTION('ref_axis',(1.,0.,0.));
#8580=DIRECTION('center_axis',(0.,0.,1.));
#8581=DIRECTION('ref_axis',(1.,0.,0.));
#8582=DIRECTION('',(0.,0.,-1.));
#8583=DIRECTION('center_axis',(0.,0.,1.));
#8584=DIRECTION('ref_axis',(1.,0.,0.));
#8585=DIRECTION('center_axis',(0.,0.,1.));
#8586=DIRECTION('ref_axis',(1.,0.,0.));
#8587=DIRECTION('center_axis',(0.,0.,1.));
#8588=DIRECTION('ref_axis',(1.,0.,0.));
#15274=CARTESIAN_POINT('',(0.,0.,0.));
#15275=CARTESIAN_POINT('Origin',(0.,0.,0.));
#15276=CARTESIAN_POINT('',(-0.294573206171349,0.000178211181277831,12.832217611709));
#15277=CARTESIAN_POINT('',(-0.294456685750782,0.000237168791136358,12.817782388291));
#15278=CARTESIAN_POINT('',(-0.2942,-3.60291088309151E-17,0.));
#15279=CARTESIAN_POINT('',(0.129212637845014,0.2648431347106,12.8));
#15280=CARTESIAN_POINT('Ctrl Pts',(-0.294573206171349,0.000178211181277831,
12.832217611709));
#15281=CARTESIAN_POINT('Ctrl Pts',(-0.294638639138964,0.00983177811479042,
12.8316935247725));
#15282=CARTESIAN_POINT('Ctrl Pts',(-0.294205630785965,0.0194791637026875,
12.831169437836));
#15283=CARTESIAN_POINT('Ctrl Pts',(-0.293254985022131,0.029074932121012,
12.8306453508995));
#15284=CARTESIAN_POINT('Ctrl Pts',(-0.283645993540782,0.126067587531217,
12.8253479550661));
#15285=CARTESIAN_POINT('Ctrl Pts',(-0.221150622395202,0.217786580006569,
12.8200505592328));
#15286=CARTESIAN_POINT('Ctrl Pts',(-0.134385324348696,0.262257101239527,
12.8147531633995));
#15287=CARTESIAN_POINT('Ctrl Pts',(-0.0538386645837653,0.303540333406841,
12.8098354422663));
#15288=CARTESIAN_POINT('Ctrl Pts',(0.0476236474357998,0.304105165469236,
12.8049177211331));
#15289=CARTESIAN_POINT('Ctrl Pts',(0.129215683241976,0.264846751495055,
12.8));
#15290=CARTESIAN_POINT('',(-0.2942,-3.60291088309151E-17,12.8));
#15291=CARTESIAN_POINT('Origin',(0.,0.,12.8));
#15292=CARTESIAN_POINT('',(-0.2942,3.60291088309151E-17,0.));
#15293=CARTESIAN_POINT('',(-0.2942,-3.60291088309151E-17,0.));
#15294=CARTESIAN_POINT('Origin',(0.,0.,0.));
#15295=CARTESIAN_POINT('',(-0.128892185405308,0.264462557919725,12.8));
#15296=CARTESIAN_POINT('Origin',(0.,0.,12.8));
#15297=CARTESIAN_POINT('Ctrl Pts',(-0.128892185405307,0.264462557919724,
12.8));
#15298=CARTESIAN_POINT('Ctrl Pts',(-0.217043456109747,0.22149991694429,
12.8053049893273));
#15299=CARTESIAN_POINT('Ctrl Pts',(-0.281220970323085,0.131282598258039,
12.8106099786547));
#15300=CARTESIAN_POINT('Ctrl Pts',(-0.292601064222616,0.0344997435524954,
12.815914967982));
#15301=CARTESIAN_POINT('Ctrl Pts',(-0.293936374384136,0.0231434990003663,
12.8165374414184));
#15302=CARTESIAN_POINT('Ctrl Pts',(-0.294544766717762,0.0116968597821011,
12.8171599148547));
#15303=CARTESIAN_POINT('Ctrl Pts',(-0.294456685750782,0.000237168791136358,
12.817782388291));
#15304=CARTESIAN_POINT('Origin',(0.,0.,0.));
#15305=CARTESIAN_POINT('',(-0.293819506992835,0.000164351555994161,12.932217611709));
#15306=CARTESIAN_POINT('',(-0.293800895129206,0.000154060581779477,12.917782388291));
#15307=CARTESIAN_POINT('',(-0.2942,-3.60291088309151E-17,0.));
#15308=CARTESIAN_POINT('Ctrl Pts',(-0.293819506992835,0.000164351555994161,
12.932217611709));
#15309=CARTESIAN_POINT('Ctrl Pts',(-0.294014132231746,0.0386044236212459,
12.9301445664391));
#15310=CARTESIAN_POINT('Ctrl Pts',(-0.287011791888666,0.0769763465444152,
12.9280715211693));
#15311=CARTESIAN_POINT('Ctrl Pts',(-0.272482130953542,0.112247367194594,
12.9259984758995));
#15312=CARTESIAN_POINT('Ctrl Pts',(-0.235353484311062,0.202377843623973,
12.9207010800661));
#15313=CARTESIAN_POINT('Ctrl Pts',(-0.149072102201679,0.272259703394973,
12.9154036842328));
#15314=CARTESIAN_POINT('Ctrl Pts',(-0.0531946070450342,0.28985545356503,
12.9101062883995));
#15315=CARTESIAN_POINT('Ctrl Pts',(0.042682888111611,0.307451203735087,
12.9048088925661));
#15316=CARTESIAN_POINT('Ctrl Pts',(0.148156496315518,0.2727608443042,12.8995114967328));
#15317=CARTESIAN_POINT('Ctrl Pts',(0.214869204494931,0.201686733123392,
12.8942141008995));
#15318=CARTESIAN_POINT('Ctrl Pts',(0.281581912674343,0.130612621942583,
12.8889167050661));
#15319=CARTESIAN_POINT('Ctrl Pts',(0.30953372082926,0.0231547590118516,
12.8836193092328));
#15320=CARTESIAN_POINT('Ctrl Pts',(0.285911633440566,-0.0714169606488347,
12.8783219133995));
#15321=CARTESIAN_POINT('Ctrl Pts',(0.262289546051872,-0.165988680309521,
12.8730245175661));
#15322=CARTESIAN_POINT('Ctrl Pts',(0.187093563119567,-0.247674256700163,
12.8677271217328));
#15323=CARTESIAN_POINT('Ctrl Pts',(0.0947944415992507,-0.279032132710234,
12.8624297258995));
#15324=CARTESIAN_POINT('Ctrl Pts',(0.00249532007893488,-0.310390008720306,
12.8571323300661));
#15325=CARTESIAN_POINT('Ctrl Pts',(-0.106906940029391,-0.291420184349807,
12.8518349342328));
#15326=CARTESIAN_POINT('Ctrl Pts',(-0.183246764174995,-0.230802112992029,
12.8465375383995));
#15327=CARTESIAN_POINT('Ctrl Pts',(-0.252034065188834,-0.176181165563425,
12.8417642295026));
#15328=CARTESIAN_POINT('Ctrl Pts',(-0.293977252056274,-0.0877450964243544,
12.8369909206058));
#15329=CARTESIAN_POINT('Ctrl Pts',(-0.294573206171349,0.000178211181277831,
12.832217611709));
#15330=CARTESIAN_POINT('Ctrl Pts',(-0.294456685750782,0.000237168791136358,
12.817782388291));
#15331=CARTESIAN_POINT('Ctrl Pts',(-0.293794102412292,-0.0859676104622492,
12.822464904182));
#15332=CARTESIAN_POINT('Ctrl Pts',(-0.253720165912887,-0.172910950724067,
12.827147420073));
#15333=CARTESIAN_POINT('Ctrl Pts',(-0.18719426584733,-0.227670130650132,
12.831829935964));
#15334=CARTESIAN_POINT('Ctrl Pts',(-0.111824699986792,-0.289708759422378,
12.8371349252914));
#15335=CARTESIAN_POINT('Ctrl Pts',(-0.00250289467999464,-0.310437626242033,
12.8424399146187));
#15336=CARTESIAN_POINT('Ctrl Pts',(0.0904196621835738,-0.280470963636124,
12.847744903946));
#15337=CARTESIAN_POINT('Ctrl Pts',(0.183342219047142,-0.250504301030214,
12.8530498932734));
#15338=CARTESIAN_POINT('Ctrl Pts',(0.259865527467481,-0.169842108998739,
12.8583548826007));
#15339=CARTESIAN_POINT('Ctrl Pts',(0.284861830842183,-0.0754928832674847,
12.863659871928));
#15340=CARTESIAN_POINT('Ctrl Pts',(0.309858134216885,0.0188563424637699,
12.8689648612554));
#15341=CARTESIAN_POINT('Ctrl Pts',(0.28332743254595,0.126892601894804,12.8742698505827));
#15342=CARTESIAN_POINT('Ctrl Pts',(0.217441929334565,0.198921329027957,
12.8795748399101));
#15343=CARTESIAN_POINT('Ctrl Pts',(0.151556426123181,0.270950056161109,
12.8848798292374));
#15344=CARTESIAN_POINT('Ctrl Pts',(0.0463161213713476,0.30697125099638,
12.8901848185647));
#15345=CARTESIAN_POINT('Ctrl Pts',(-0.0498919590377675,0.290443329283603,
12.8954898078921));
#15346=CARTESIAN_POINT('Ctrl Pts',(-0.146100039446882,0.273915407570827,
12.9007947972194));
#15347=CARTESIAN_POINT('Ctrl Pts',(-0.233275895513279,0.204838369310003,
12.9060997865467));
#15348=CARTESIAN_POINT('Ctrl Pts',(-0.271352858586062,0.114956956369256,
12.9114047758741));
#15349=CARTESIAN_POINT('Ctrl Pts',(-0.286611457457756,0.0789387365479301,
12.9135306466797));
#15350=CARTESIAN_POINT('Ctrl Pts',(-0.29398551548852,0.0395796482908291,
12.9156565174854));
#15351=CARTESIAN_POINT('Ctrl Pts',(-0.293800895129206,0.000154060581779477,
12.917782388291));
#15352=CARTESIAN_POINT('Origin',(0.,0.,0.));
#15353=CARTESIAN_POINT('',(-0.293978383054635,-0.000241987351228545,13.032217611709));
#15354=CARTESIAN_POINT('',(-0.293977558237541,-0.000244103523127173,13.017782388291));
#15355=CARTESIAN_POINT('',(-0.2942,-3.60291088309151E-17,0.));
#15356=CARTESIAN_POINT('Ctrl Pts',(-0.293978383054635,-0.000241987351228545,
13.032217611709));
#15357=CARTESIAN_POINT('Ctrl Pts',(-0.293459536795742,0.0668289020834338,
13.0285956081058));
#15358=CARTESIAN_POINT('Ctrl Pts',(-0.270690894883612,0.134218310941281,
13.0249736045026));
#15359=CARTESIAN_POINT('Ctrl Pts',(-0.22864087855502,0.18592830985058,13.0213516008995));
#15360=CARTESIAN_POINT('Ctrl Pts',(-0.167140227065884,0.261557260778287,
13.0160542050661));
#15361=CARTESIAN_POINT('Ctrl Pts',(-0.0643951667298436,0.303646694219936,
13.0107568092328));
#15362=CARTESIAN_POINT('Ctrl Pts',(0.0324891899508726,0.292900047757626,
13.0054594133995));
#15363=CARTESIAN_POINT('Ctrl Pts',(0.129373546631589,0.282153401295317,
13.0001620175661));
#15364=CARTESIAN_POINT('Ctrl Pts',(0.220397199656981,0.218570674929048,
12.9948646217328));
#15365=CARTESIAN_POINT('Ctrl Pts',(0.263828885312461,0.131302362204768,
12.9895672258995));
#15366=CARTESIAN_POINT('Ctrl Pts',(0.307260570967942,0.0440340494804873,
12.9842698300661));
#15367=CARTESIAN_POINT('Ctrl Pts',(0.30310028925351,-0.0669198496018051,
12.9789724342328));
#15368=CARTESIAN_POINT('Ctrl Pts',(0.253255413164487,-0.150690690040053,
12.9736750383995));
#15369=CARTESIAN_POINT('Ctrl Pts',(0.203410537075464,-0.2344615304783,12.9683776425661));
#15370=CARTESIAN_POINT('Ctrl Pts',(0.10788106661185,-0.291049312272503,
12.9630802467328));
#15371=CARTESIAN_POINT('Ctrl Pts',(0.0104639653641406,-0.294510570060203,
12.9577828508995));
#15372=CARTESIAN_POINT('Ctrl Pts',(-0.0869531358835682,-0.297971827847904,
12.9524854550661));
#15373=CARTESIAN_POINT('Ctrl Pts',(-0.186257867915372,-0.248306561629102,
12.9471880592328));
#15374=CARTESIAN_POINT('Ctrl Pts',(-0.241922278343485,-0.168284381975822,
12.9418906633995));
#15375=CARTESIAN_POINT('Ctrl Pts',(-0.275803373654782,-0.119577513889043,
12.938666312836));
#15376=CARTESIAN_POINT('Ctrl Pts',(-0.29351679290941,-0.0596241488826022,
12.9354419622725));
#15377=CARTESIAN_POINT('Ctrl Pts',(-0.293819506992835,0.000164351555994161,
12.932217611709));
#15378=CARTESIAN_POINT('Ctrl Pts',(-0.293800895129206,0.000154060581779477,
12.917782388291));
#15379=CARTESIAN_POINT('Ctrl Pts',(-0.293524805913338,-0.0588046568438365,
12.9209615068127));
#15380=CARTESIAN_POINT('Ctrl Pts',(-0.276344869041408,-0.117912090294522,
12.9241406253344));
#15381=CARTESIAN_POINT('Ctrl Pts',(-0.243350877161725,-0.166217658514054,
12.9273197438561));
#15382=CARTESIAN_POINT('Ctrl Pts',(-0.188293862585438,-0.246825072835943,
12.9326247331834));
#15383=CARTESIAN_POINT('Ctrl Pts',(-0.0892017633536947,-0.29735411385905,
12.9379297225108));
#15384=CARTESIAN_POINT('Ctrl Pts',(0.00837448788296055,-0.294579959740858,
12.9432347118381));
#15385=CARTESIAN_POINT('Ctrl Pts',(0.105950739119616,-0.291805805622667,
12.9485397011654));
#15386=CARTESIAN_POINT('Ctrl Pts',(0.202011142361183,-0.235728456363176,
12.9538446904928));
#15387=CARTESIAN_POINT('Ctrl Pts',(0.252400245841885,-0.152124079723166,
12.9591496798201));
#15388=CARTESIAN_POINT('Ctrl Pts',(0.302789349322588,-0.068519703083155,
12.9644546691475));
#15389=CARTESIAN_POINT('Ctrl Pts',(0.307507153042424,0.0426117009373751,
12.9697596584748));
#15390=CARTESIAN_POINT('Ctrl Pts',(0.264384723644278,0.130185938245225,
12.9750646478021));
#15391=CARTESIAN_POINT('Ctrl Pts',(0.221262294246132,0.217760175553074,
12.9803696371295));
#15392=CARTESIAN_POINT('Ctrl Pts',(0.130299631730003,0.281777246148244,
12.9856746264568));
#15393=CARTESIAN_POINT('Ctrl Pts',(0.0333096771051611,0.292810643338737,
12.9909796157841));
#15394=CARTESIAN_POINT('Ctrl Pts',(-0.0636802775196813,0.303844040529229,
12.9962846051115));
#15395=CARTESIAN_POINT('Ctrl Pts',(-0.166697524253236,0.261893764315045,
13.0015895944388));
#15396=CARTESIAN_POINT('Ctrl Pts',(-0.228388209822111,0.186242989953447,
13.0068945837661));
#15397=CARTESIAN_POINT('Ctrl Pts',(-0.270592261142874,0.134488513014659,
13.0105238519411));
#15398=CARTESIAN_POINT('Ctrl Pts',(-0.293454446900826,0.0669613589840213,
13.0141531201161));
#15399=CARTESIAN_POINT('Ctrl Pts',(-0.293977558237541,-0.000244103523127173,
13.017782388291));
#15400=CARTESIAN_POINT('Origin',(0.,0.,0.));
#15401=CARTESIAN_POINT('',(-0.294688566460017,-4.3425772024458E-5,13.132217611709));
#15402=CARTESIAN_POINT('',(-0.294684770789603,-5.92838055088064E-5,13.117782388291));
#15403=CARTESIAN_POINT('',(-0.2942,-3.60291088309151E-17,0.));
#15404=CARTESIAN_POINT('Ctrl Pts',(-0.294688566460017,-4.3425772024458E-5,
13.132217611709));
#15405=CARTESIAN_POINT('Ctrl Pts',(-0.294492695162095,0.0951154314666305,
13.1270466497725));
#15406=CARTESIAN_POINT('Ctrl Pts',(-0.244188233801183,0.190452094564122,
13.121875687836));
#15407=CARTESIAN_POINT('Ctrl Pts',(-0.165446572490844,0.243871726854215,
13.1167047258995));
#15408=CARTESIAN_POINT('Ctrl Pts',(-0.0847796185164032,0.298597509210938,
13.1114073300661));
#15409=CARTESIAN_POINT('Ctrl Pts',(0.0257321580046905,0.309331395447293,
13.1061099342328));
#15410=CARTESIAN_POINT('Ctrl Pts',(0.115422863317555,0.271152263674646,
13.1008125383995));
#15411=CARTESIAN_POINT('Ctrl Pts',(0.205113568630419,0.232973131901999,
13.0955151425661));
#15412=CARTESIAN_POINT('Ctrl Pts',(0.273983202735053,0.145880982120351,
13.0902177467328));
#15413=CARTESIAN_POINT('Ctrl Pts',(0.290457378744519,0.049804604878551,
13.0849203508995));
#15414=CARTESIAN_POINT('Ctrl Pts',(0.306931554753985,-0.0462717723632486,
13.0796229550661));
#15415=CARTESIAN_POINT('Ctrl Pts',(0.271010272668282,-0.1513323770652,13.0743255592328));
#15416=CARTESIAN_POINT('Ctrl Pts',(0.19916221987775,-0.217210491733346,
13.0690281633995));
#15417=CARTESIAN_POINT('Ctrl Pts',(0.127314167087218,-0.283088606401493,
13.0637307675661));
#15418=CARTESIAN_POINT('Ctrl Pts',(0.0195393435918585,-0.309784231035834,
13.0584333717328));
#15419=CARTESIAN_POINT('Ctrl Pts',(-0.0747511573933412,-0.285058330392084,
13.0531359758995));
#15420=CARTESIAN_POINT('Ctrl Pts',(-0.169041658378541,-0.260332429748335,
13.0478385800661));
#15421=CARTESIAN_POINT('Ctrl Pts',(-0.24984783685358,-0.184185003826495,
13.0425411842328));
#15422=CARTESIAN_POINT('Ctrl Pts',(-0.280122804769983,-0.0915270566586923,
13.0372437883995));
#15423=CARTESIAN_POINT('Ctrl Pts',(-0.289697782289419,-0.0622223927007149,
13.0355683961693));
#15424=CARTESIAN_POINT('Ctrl Pts',(-0.294218380328531,-0.0312662654416913,
13.0338930039391));
#15425=CARTESIAN_POINT('Ctrl Pts',(-0.293978383054635,-0.000241987351228545,
13.032217611709));
#15426=CARTESIAN_POINT('Ctrl Pts',(-0.293977558237541,-0.000244103523127173,
13.017782388291));
#15427=CARTESIAN_POINT('Ctrl Pts',(-0.294219091430933,-0.0312744957809374,
13.0194581094434));
#15428=CARTESIAN_POINT('Ctrl Pts',(-0.289698173215612,-0.0622363068513482,
13.0211338305958));
#15429=CARTESIAN_POINT('Ctrl Pts',(-0.280119774337342,-0.091545292928116,
13.0228095517481));
#15430=CARTESIAN_POINT('Ctrl Pts',(-0.249796528879502,-0.184331528939066,
13.0281145410755));
#15431=CARTESIAN_POINT('Ctrl Pts',(-0.168785913559629,-0.260552728451954,
13.0334195304028));
#15432=CARTESIAN_POINT('Ctrl Pts',(-0.0743260837926121,-0.285172326966721,
13.0387245197302));
#15433=CARTESIAN_POINT('Ctrl Pts',(0.0201337459744046,-0.309791925481488,
13.0440295090575));
#15434=CARTESIAN_POINT('Ctrl Pts',(0.128042790188565,-0.282809922998135,
13.0493344983848));
#15435=CARTESIAN_POINT('Ctrl Pts',(0.199798520936279,-0.216629121303023,
13.0546394877122));
#15436=CARTESIAN_POINT('Ctrl Pts',(0.271554251683993,-0.150448319607911,
13.0599444770395));
#15437=CARTESIAN_POINT('Ctrl Pts',(0.307156668965259,-0.0450687187010392,
13.0652494663668));
#15438=CARTESIAN_POINT('Ctrl Pts',(0.290240410451035,0.0510698486205661,
13.0705544556942));
#15439=CARTESIAN_POINT('Ctrl Pts',(0.273324151936811,0.147208415942171,
13.0758594450215));
#15440=CARTESIAN_POINT('Ctrl Pts',(0.203889217627098,0.23410594967851,13.0811644343489));
#15441=CARTESIAN_POINT('Ctrl Pts',(0.113852756432599,0.271818274816414,
13.0864694236762));
#15442=CARTESIAN_POINT('Ctrl Pts',(0.0238162952380993,0.309530599954319,
13.0917744130035));
#15443=CARTESIAN_POINT('Ctrl Pts',(-0.0868216928411871,0.29805771649379,
13.0970794023309));
#15444=CARTESIAN_POINT('Ctrl Pts',(-0.16720425947304,0.242673361913228,
13.1023843916582));
#15445=CARTESIAN_POINT('Ctrl Pts',(-0.244975731695611,0.189088076268463,
13.1075170572025));
#15446=CARTESIAN_POINT('Ctrl Pts',(-0.294425452342338,0.09439776822128,
13.1126497227468));
#15447=CARTESIAN_POINT('Ctrl Pts',(-0.294684770789603,-5.92838055088064E-5,
13.117782388291));
#15448=CARTESIAN_POINT('Origin',(0.,0.,0.));
#15449=CARTESIAN_POINT('',(-0.294107431028703,0.000266555779104893,13.232217611709));
#15450=CARTESIAN_POINT('',(-0.294157826435532,0.000271978496102963,13.217782388291));
#15451=CARTESIAN_POINT('',(-0.2942,-3.60291088309151E-17,0.));
#15452=CARTESIAN_POINT('Ctrl Pts',(-0.294107431028703,0.000266555779104893,
13.232217611709));
#15453=CARTESIAN_POINT('Ctrl Pts',(-0.294339337791913,0.026579066670166,
13.2307950872725));
#15454=CARTESIAN_POINT('Ctrl Pts',(-0.29110065943816,0.0528354654390751,
13.229372562836));
#15455=CARTESIAN_POINT('Ctrl Pts',(-0.28416559484468,0.0780762592101134,
13.2279500383995));
#15456=CARTESIAN_POINT('Ctrl Pts',(-0.258339829508931,0.172071464017823,
13.2226526425661));
#15457=CARTESIAN_POINT('Ctrl Pts',(-0.181253577517488,0.251982532843938,
13.2173552467328));
#15458=CARTESIAN_POINT('Ctrl Pts',(-0.0882482661206186,0.281172955778023,
13.2120578508995));
#15459=CARTESIAN_POINT('Ctrl Pts',(0.00475704527625133,0.310363378712107,
13.2067604550661));
#15460=CARTESIAN_POINT('Ctrl Pts',(0.113681416078549,0.288833155754161,
13.2014630592328));
#15461=CARTESIAN_POINT('Ctrl Pts',(0.1885867242503,0.226453162726531,13.1961656633995));
#15462=CARTESIAN_POINT('Ctrl Pts',(0.263492032422051,0.164073169698901,
13.1908682675661));
#15463=CARTESIAN_POINT('Ctrl Pts',(0.304378277963256,0.0608434066015877,
13.1855708717328));
#15464=CARTESIAN_POINT('Ctrl Pts',(0.292500506687337,-0.035908788554837,
13.1802734758995));
#15465=CARTESIAN_POINT('Ctrl Pts',(0.280622735411417,-0.132660983711262,
13.1749760800661));
#15466=CARTESIAN_POINT('Ctrl Pts',(0.215980947318375,-0.222935610926797,
13.1696786842328));
#15467=CARTESIAN_POINT('Ctrl Pts',(0.128211205478304,-0.265344821495433,
13.1643812883995));
#15468=CARTESIAN_POINT('Ctrl Pts',(0.0404414636382319,-0.307754032064069,
13.1590838925661));
#15469=CARTESIAN_POINT('Ctrl Pts',(-0.0704562319488692,-0.302297825985805,
13.1537864967328));
#15470=CARTESIAN_POINT('Ctrl Pts',(-0.153639056706568,-0.251477688371532,
13.1484891008995));
#15471=CARTESIAN_POINT('Ctrl Pts',(-0.236821881464266,-0.200657550757259,
13.1431917050661));
#15472=CARTESIAN_POINT('Ctrl Pts',(-0.292289835392562,-0.104473481606977,
13.1378943092328));
#15473=CARTESIAN_POINT('Ctrl Pts',(-0.294612746642817,-0.00702260779328966,
13.1325969133995));
#15474=CARTESIAN_POINT('Ctrl Pts',(-0.294668187982413,-0.0046967303029458,
13.1324704795026));
#15475=CARTESIAN_POINT('Ctrl Pts',(-0.294693355660127,-0.00237013118713854,
13.1323440456058));
#15476=CARTESIAN_POINT('Ctrl Pts',(-0.294688566460017,-4.3425772024458E-5,
13.132217611709));
#15477=CARTESIAN_POINT('Ctrl Pts',(-0.294684770789603,-5.92838055088064E-5,
13.117782388291));
#15478=CARTESIAN_POINT('Ctrl Pts',(-0.294693477130483,-0.00323057879859576,
13.1179547120741));
#15479=CARTESIAN_POINT('Ctrl Pts',(-0.294646735599431,-0.00640161086335999,
13.1181270358572));
#15480=CARTESIAN_POINT('Ctrl Pts',(-0.294543756425539,-0.00957081555894318,
13.1182993596402));
#15481=CARTESIAN_POINT('Ctrl Pts',(-0.291373541561766,-0.107134812749959,
13.1236043489676));
#15482=CARTESIAN_POINT('Ctrl Pts',(-0.234905966649797,-0.202966981431395,
13.1289093382949));
#15483=CARTESIAN_POINT('Ctrl Pts',(-0.151097474548945,-0.253016161695952,
13.1342143276222));
#15484=CARTESIAN_POINT('Ctrl Pts',(-0.0672889824480926,-0.303065341960509,
13.1395193169496));
#15485=CARTESIAN_POINT('Ctrl Pts',(0.0438604268416431,-0.307331533808189,
13.1448243062769));
#15486=CARTESIAN_POINT('Ctrl Pts',(0.131258719251342,-0.26385369724767,
13.1501292956042));
#15487=CARTESIAN_POINT('Ctrl Pts',(0.218657011661041,-0.220375860687151,
13.1554342849316));
#15488=CARTESIAN_POINT('Ctrl Pts',(0.282304187190703,-0.129153995718433,
13.1607392742589));
#15489=CARTESIAN_POINT('Ctrl Pts',(0.292943557088177,-0.0321200449435113,
13.1660442635862));
#15490=CARTESIAN_POINT('Ctrl Pts',(0.30358292698565,0.0649139058314107,
13.1713492529136));
#15491=CARTESIAN_POINT('Ctrl Pts',(0.261214491250936,0.167759942412537,
13.1766542422409));
#15492=CARTESIAN_POINT('Ctrl Pts',(0.18531374311845,0.229142840892087,13.1819592315683));
#15493=CARTESIAN_POINT('Ctrl Pts',(0.109412994985964,0.290525739371636,
13.1872642208956));
#15494=CARTESIAN_POINT('Ctrl Pts',(-2.00655442916947E-5,0.31044549974961,
13.1925692102229));
#15495=CARTESIAN_POINT('Ctrl Pts',(-0.0926823581075636,0.27974560840399,
13.1978741995503));
#15496=CARTESIAN_POINT('Ctrl Pts',(-0.185344650670836,0.249045717058369,
13.2031791888776));
#15497=CARTESIAN_POINT('Ctrl Pts',(-0.261236175267123,0.167726173989153,
13.2084841782049));
#15498=CARTESIAN_POINT('Ctrl Pts',(-0.285471884901514,0.0731671227495215,
13.2137891675323));
#15499=CARTESIAN_POINT('Ctrl Pts',(-0.291552860931422,0.0494413341230131,
13.2151202411185));
#15500=CARTESIAN_POINT('Ctrl Pts',(-0.294381808637396,0.0248820429063915,
13.2164513147048));
#15501=CARTESIAN_POINT('Ctrl Pts',(-0.294157826435532,0.000271978496102963,
13.217782388291));
#15502=CARTESIAN_POINT('Origin',(0.,0.,0.));
#15503=CARTESIAN_POINT('',(-0.293756705318437,-9.65891231691218E-5,13.332217611709));
#15504=CARTESIAN_POINT('',(-0.293733177601347,-5.56197620117739E-5,13.317782388291));
#15505=CARTESIAN_POINT('',(-0.2942,-3.60291088309151E-17,0.));
#15506=CARTESIAN_POINT('Ctrl Pts',(-0.293756705318437,-9.65891231691218E-5,
13.332217611709));
#15507=CARTESIAN_POINT('Ctrl Pts',(-0.29359459382837,0.0550324553525043,
13.3292461289391));
#15508=CARTESIAN_POINT('Ctrl Pts',(-0.27871547764323,0.110242707595751,
13.3262746461693));
#15509=CARTESIAN_POINT('Ctrl Pts',(-0.249665643167405,0.156566455486698,
13.3233031633995));
#15510=CARTESIAN_POINT('Ctrl Pts',(-0.197877198127916,0.23914988203496,
13.3180057675661));
#15511=CARTESIAN_POINT('Ctrl Pts',(-0.101051667078895,0.29349040285122,
13.3127083717328));
#15512=CARTESIAN_POINT('Ctrl Pts',(-0.0035803010767538,0.294674689259135,
13.3074109758995));
#15513=CARTESIAN_POINT('Ctrl Pts',(0.093891064925387,0.295858975667049,
13.3021135800661));
#15514=CARTESIAN_POINT('Ctrl Pts',(0.192008265880649,0.243887027666619,
13.2968161842328));
#15515=CARTESIAN_POINT('Ctrl Pts',(0.245787916885835,0.162586239740655,
13.2915187883995));
#15516=CARTESIAN_POINT('Ctrl Pts',(0.299567567891021,0.081285451814691,
13.2862213925661));
#15517=CARTESIAN_POINT('Ctrl Pts',(0.30900966894613,-0.0293441760368059,
13.2809239967328));
#15518=CARTESIAN_POINT('Ctrl Pts',(0.269785329248371,-0.118582730077581,
13.2756266008995));
#15519=CARTESIAN_POINT('Ctrl Pts',(0.230560989550612,-0.207821284118357,
13.2703292050661));
#15520=CARTESIAN_POINT('Ctrl Pts',(0.142670209099985,-0.275668764348411,
13.2650318092328));
#15521=CARTESIAN_POINT('Ctrl Pts',(0.0464079278430225,-0.291019401563061,
13.2597344133995));
#15522=CARTESIAN_POINT('Ctrl Pts',(-0.0498543534139403,-0.306370038777712,
13.2544370175661));
#15523=CARTESIAN_POINT('Ctrl Pts',(-0.154488135477239,-0.269223832976959,
13.2491396217328));
#15524=CARTESIAN_POINT('Ctrl Pts',(-0.219522387168861,-0.196611059681931,
13.2438422258995));
#15525=CARTESIAN_POINT('Ctrl Pts',(-0.267092810377316,-0.143497196353984,
13.2399673545026));
#15526=CARTESIAN_POINT('Ctrl Pts',(-0.293475730890246,-0.0714071485275604,
13.2360924831058));
#15527=CARTESIAN_POINT('Ctrl Pts',(-0.294107431028703,0.000266555779104893,
13.232217611709));
#15528=CARTESIAN_POINT('Ctrl Pts',(-0.294157826435532,0.000271978496102963,
13.217782388291));
#15529=CARTESIAN_POINT('Ctrl Pts',(-0.293489128320791,-0.0732012865127652,
13.2217563040321));
#15530=CARTESIAN_POINT('Ctrl Pts',(-0.265609085010938,-0.147127102658161,
13.2257302197732));
#15531=CARTESIAN_POINT('Ctrl Pts',(-0.21581576504657,-0.200676806043974,
13.2297041355143));
#15532=CARTESIAN_POINT('Ctrl Pts',(-0.14934404088474,-0.272163124187789,
13.2350091248416));
#15533=CARTESIAN_POINT('Ctrl Pts',(-0.0438206978885843,-0.307337201065372,
13.240314114169));
#15534=CARTESIAN_POINT('Ctrl Pts',(0.0522483628297525,-0.290030573409733,
13.2456191034963));
#15535=CARTESIAN_POINT('Ctrl Pts',(0.14831742354809,-0.272723945754094,
13.2509240928236));
#15536=CARTESIAN_POINT('Ctrl Pts',(0.234932201988608,-0.202936613565231,
13.256229082151));
#15537=CARTESIAN_POINT('Ctrl Pts',(0.272278494649526,-0.112747710601187,
13.2615340714783));
#15538=CARTESIAN_POINT('Ctrl Pts',(0.309624787310445,-0.022558807637142,
13.2668390608057));
#15539=CARTESIAN_POINT('Ctrl Pts',(0.297702594191763,0.0880316661020849,
13.272144050133));
#15540=CARTESIAN_POINT('Ctrl Pts',(0.241992187856524,0.168188602396665,
13.2774490394603));
#15541=CARTESIAN_POINT('Ctrl Pts',(0.186281781521285,0.248345538691245,
13.2827540287877));
#15542=CARTESIAN_POINT('Ctrl Pts',(0.0867831619694888,0.298068937541179,
13.288059018115));
#15543=CARTESIAN_POINT('Ctrl Pts',(-0.0107671528494052,0.294502450563172,
13.2933640074423));
#15544=CARTESIAN_POINT('Ctrl Pts',(-0.108317467668299,0.290935963585165,
13.2986689967697));
#15545=CARTESIAN_POINT('Ctrl Pts',(-0.203919477754291,0.234079590779218,
13.303973986097));
#15546=CARTESIAN_POINT('Ctrl Pts',(-0.253627821392627,0.150068493985587,
13.3092789754243));
#15547=CARTESIAN_POINT('Ctrl Pts',(-0.280187131430457,0.105181124923475,
13.3121134463799));
#15548=CARTESIAN_POINT('Ctrl Pts',(-0.293644738529364,0.052541637658281,
13.3149479173355));
#15549=CARTESIAN_POINT('Ctrl Pts',(-0.293733177601347,-5.56197620117739E-5,
13.317782388291));
#15550=CARTESIAN_POINT('Origin',(0.,0.,0.));
#15551=CARTESIAN_POINT('',(-0.294460332090693,-0.000220795745557084,13.432217611709));
#15552=CARTESIAN_POINT('',(-0.294362671296069,-0.000253937998619662,13.417782388291));
#15553=CARTESIAN_POINT('',(-0.2942,-3.60291088309151E-17,0.));
#15554=CARTESIAN_POINT('Ctrl Pts',(-0.294460332090693,-0.000220795745557084,
13.432217611709));
#15555=CARTESIAN_POINT('Ctrl Pts',(-0.293757341683982,0.0831358178453026,
13.4276971706058));
#15556=CARTESIAN_POINT('Ctrl Pts',(-0.25664007441063,0.167036070084589,
13.4231767295026));
#15557=CARTESIAN_POINT('Ctrl Pts',(-0.194033810233309,0.221803347340193,
13.4186562883995));
#15558=CARTESIAN_POINT('Ctrl Pts',(-0.120667040171587,0.285983797812974,
13.4133588925661));
#15559=CARTESIAN_POINT('Ctrl Pts',(-0.0122964079182814,0.310156136338401,
13.4080614967328));
#15560=CARTESIAN_POINT('Ctrl Pts',(0.0813910654447742,0.283234545604937,
13.4027641008995));
#15561=CARTESIAN_POINT('Ctrl Pts',(0.17507853880783,0.256312954871473,13.3974667050661));
#15562=CARTESIAN_POINT('Ctrl Pts',(0.254082853280636,0.178297434879117,
13.3921693092328));
#15563=CARTESIAN_POINT('Ctrl Pts',(0.28218455619408,0.0849572034945515,
13.3868719133995));
#15564=CARTESIAN_POINT('Ctrl Pts',(0.310286259107524,-0.00838302789001326,
13.3815745175661));
#15565=CARTESIAN_POINT('Ctrl Pts',(0.287485350461608,-0.117047970666788,
13.3762771217328));
#15566=CARTESIAN_POINT('Ctrl Pts',(0.224234622987472,-0.191219290305052,
13.3709797258995));
#15567=CARTESIAN_POINT('Ctrl Pts',(0.160983895513336,-0.265390609943316,
13.3656823300661));
#15568=CARTESIAN_POINT('Ctrl Pts',(0.0572833492109803,-0.305068306443069,
13.3603849342328));
#15569=CARTESIAN_POINT('Ctrl Pts',(-0.0393235254694371,-0.292061093472824,
13.3550875383995));
#15570=CARTESIAN_POINT('Ctrl Pts',(-0.135930400149854,-0.279053880502579,
13.3497901425661));
#15571=CARTESIAN_POINT('Ctrl Pts',(-0.225443603208334,-0.213361758062335,
13.3444927467328));
#15572=CARTESIAN_POINT('Ctrl Pts',(-0.266824525222594,-0.125102530702081,
13.3391953508995));
#15573=CARTESIAN_POINT('Ctrl Pts',(-0.284993533188177,-0.0863507937448422,
13.336869437836));
#15574=CARTESIAN_POINT('Ctrl Pts',(-0.293883597264882,-0.0432485690121582,
13.3345435247725));
#15575=CARTESIAN_POINT('Ctrl Pts',(-0.293756705318437,-9.65891231691218E-5,
13.332217611709));
#15576=CARTESIAN_POINT('Ctrl Pts',(-0.293733177601347,-5.56197620117739E-5,
13.317782388291));
#15577=CARTESIAN_POINT('Ctrl Pts',(-0.293810260893271,-0.0458992684706001,
13.3202529066628));
#15578=CARTESIAN_POINT('Ctrl Pts',(-0.28373102046765,-0.0917108359027396,
13.3227234250346));
#15579=CARTESIAN_POINT('Ctrl Pts',(-0.263318357641365,-0.132329391391207,
13.3251939434064));
#15580=CARTESIAN_POINT('Ctrl Pts',(-0.219485873061089,-0.219550359193053,
13.3304989327337));
#15581=CARTESIAN_POINT('Ctrl Pts',(-0.12800622670986,-0.282826474015431,
13.335803922061));
#15582=CARTESIAN_POINT('Ctrl Pts',(-0.0309298619793288,-0.29307161036645,
13.3411089113884));
#15583=CARTESIAN_POINT('Ctrl Pts',(0.0661465027512023,-0.303316746717469,
13.3464139007157));
#15584=CARTESIAN_POINT('Ctrl Pts',(0.168819585861035,-0.260530904597129,
13.351718890043));
#15585=CARTESIAN_POINT('Ctrl Pts',(0.229893678370732,-0.184381450923717,
13.3570238793704));
#15586=CARTESIAN_POINT('Ctrl Pts',(0.290967770880429,-0.108231997250306,
13.3623288686977));
#15587=CARTESIAN_POINT('Ctrl Pts',(0.31044287278999,0.00128106797617772,
13.3676338580251));
#15588=CARTESIAN_POINT('Ctrl Pts',(0.27936683882728,0.0938178980565548,
13.3729388473524));
#15589=CARTESIAN_POINT('Ctrl Pts',(0.24829080486457,0.186354728136933,13.3782438366797));
#15590=CARTESIAN_POINT('Ctrl Pts',(0.166663635029587,0.261915323071205,
13.3835488260071));
#15591=CARTESIAN_POINT('Ctrl Pts',(0.0720069368793092,0.285766734827215,
13.3888538153344));
#15592=CARTESIAN_POINT('Ctrl Pts',(-0.0226497612709665,0.309618146583224,
13.3941588046617));
#15593=CARTESIAN_POINT('Ctrl Pts',(-0.130335987736536,0.281760375160974,
13.3994637939891));
#15594=CARTESIAN_POINT('Ctrl Pts',(-0.201551747218579,0.214998838681592,
13.4047687833164));
#15595=CARTESIAN_POINT('Ctrl Pts',(-0.259784585821543,0.160408200219468,
13.4091066516413));
#15596=CARTESIAN_POINT('Ctrl Pts',(-0.293632297236924,0.0798054665620052,
13.4134445199662));
#15597=CARTESIAN_POINT('Ctrl Pts',(-0.294362671296069,-0.000253937998619662,
13.417782388291));
#15598=CARTESIAN_POINT('Origin',(0.,0.,12.6151410108095));
#15599=CARTESIAN_POINT('',(-0.237384871732189,-0.000177998745596757,13.4651410108095));
#15600=CARTESIAN_POINT('',(-0.237480735682898,0.000138191412729517,13.4848589891905));
#15601=CARTESIAN_POINT('',(-0.237175,-1.00305832390001E-14,12.6151410108095));
#15602=CARTESIAN_POINT('',(-0.234668236863855,0.0343918483395353,13.562825));
#15603=CARTESIAN_POINT('Ctrl Pts',(-0.237384871732189,-0.000177998745596738,
13.4651410108095));
#15604=CARTESIAN_POINT('Ctrl Pts',(-0.237482278815476,-0.0117279779843829,
13.4659179655397));
#15605=CARTESIAN_POINT('Ctrl Pts',(-0.23146378830816,-0.101926256035546,
13.4719923161032));
#15606=CARTESIAN_POINT('Ctrl Pts',(-0.115844693426342,-0.255404084499389,
13.4833640625));
#15607=CARTESIAN_POINT('Ctrl Pts',(0.151994963678255,-0.235653121630174,
13.49925625));
#15608=CARTESIAN_POINT('Ctrl Pts',(0.280386067331958,7.16919272130007E-5,
13.5151484375));
#15609=CARTESIAN_POINT('Ctrl Pts',(0.151848011613721,0.23594581398157,13.531040625));
#15610=CARTESIAN_POINT('Ctrl Pts',(-0.116259094268414,0.255025114686607,
13.5469328125));
#15611=CARTESIAN_POINT('Ctrl Pts',(-0.223221075339677,0.112500043789072,
13.5575276041667));
#15612=CARTESIAN_POINT('Ctrl Pts',(-0.234668236863856,0.0343918483395283,
13.562825));
#15613=CARTESIAN_POINT('',(-0.0439445221993903,0.233068358199193,13.562825));
#15614=CARTESIAN_POINT('Origin',(0.,0.,13.562825));
#15615=CARTESIAN_POINT('Ctrl Pts',(-0.237480735682898,0.000138191412729494,
13.4848589891905));
#15616=CARTESIAN_POINT('Ctrl Pts',(-0.236987434834035,-0.0706816697969668,
13.489627702151));
#15617=CARTESIAN_POINT('Ctrl Pts',(-0.165686680756775,-0.221141686642749,
13.4997014044388));
#15618=CARTESIAN_POINT('Ctrl Pts',(0.0903269506402298,-0.265580501456578,
13.515080096054));
#15619=CARTESIAN_POINT('Ctrl Pts',(0.272486967933624,-0.0674994743880085,
13.530995064036));
#15620=CARTESIAN_POINT('Ctrl Pts',(0.203600577200948,0.19281335099551,13.546910032018));
#15621=CARTESIAN_POINT('Ctrl Pts',(0.0337423613347716,0.2477160478489,13.5575200106727));
#15622=CARTESIAN_POINT('Ctrl Pts',(-0.043944522199392,0.233068358199193,
13.562825));
#15623=CARTESIAN_POINT('Origin',(0.,0.,12.6151410108095));
#15624=CARTESIAN_POINT('',(-0.236817629449015,-7.78671831719857E-5,13.3651410108095));
#15625=CARTESIAN_POINT('',(-0.237306140600426,-0.000204717011637295,13.3848589891905));
#15626=CARTESIAN_POINT('',(-0.237175,-1.00305832390001E-14,12.6151410108095));
#15627=CARTESIAN_POINT('Ctrl Pts',(-0.236817629449016,-7.78671831719799E-5,
13.3651410108095));
#15628=CARTESIAN_POINT('Ctrl Pts',(-0.236919925837179,-0.0348656674216854,
13.367466923873));
#15629=CARTESIAN_POINT('Ctrl Pts',(-0.213430025619855,-0.148753143302577,
13.3750902327698));
#15630=CARTESIAN_POINT('Ctrl Pts',(-0.0374201180154527,-0.277923634425439,
13.3880109375));
#15631=CARTESIAN_POINT('Ctrl Pts',(0.213380463928066,-0.18196281524805,
13.403903125));
#15632=CARTESIAN_POINT('Ctrl Pts',(0.268524639741408,0.0808441983795663,
13.4197953125));
#15633=CARTESIAN_POINT('Ctrl Pts',(0.077452087548127,0.269525343391667,
13.4356875));
#15634=CARTESIAN_POINT('Ctrl Pts',(-0.171829534519279,0.213922458814076,
13.4508027327698));
#15635=CARTESIAN_POINT('Ctrl Pts',(-0.236818142467366,0.0670215417996536,
13.4606205697063));
#15636=CARTESIAN_POINT('Ctrl Pts',(-0.237384871732189,-0.000177998745596738,
13.4651410108095));
#15637=CARTESIAN_POINT('Ctrl Pts',(-0.237306140600426,-0.000204717011637273,
13.3848589891905));
#15638=CARTESIAN_POINT('Ctrl Pts',(-0.23743741378788,-0.0145941289722833,
13.385826110193));
#15639=CARTESIAN_POINT('Ctrl Pts',(-0.229682327632944,-0.107773186042249,
13.3920982205228));
#15640=CARTESIAN_POINT('Ctrl Pts',(-0.106286584194727,-0.259655320928406,
13.4036753201799));
#15641=CARTESIAN_POINT('Ctrl Pts',(0.161056632784338,-0.229734753162831,
13.4195902881619));
#15642=CARTESIAN_POINT('Ctrl Pts',(0.280337460803119,0.0113889577443968,
13.4355052561439));
#15643=CARTESIAN_POINT('Ctrl Pts',(0.141885966824002,0.242044705653255,
13.4514202241259));
#15644=CARTESIAN_POINT('Ctrl Pts',(-0.126992591218768,0.250174275017661,
13.4673351921079));
#15645=CARTESIAN_POINT('Ctrl Pts',(-0.233558987596684,0.0947948497711226,
13.4784814471295));
#15646=CARTESIAN_POINT('Ctrl Pts',(-0.237536210941985,0.00810239856573657,
13.4843227128237));
#15647=CARTESIAN_POINT('Ctrl Pts',(-0.237480735682898,0.000138191412729494,
13.4848589891905));
#15648=CARTESIAN_POINT('Origin',(0.,0.,12.6151410108095));
#15649=CARTESIAN_POINT('',(-0.237100373739744,0.000214889078547364,13.2651410108095));
#15650=CARTESIAN_POINT('',(-0.236798662126443,-4.48389431123158E-5,13.2848589891905));
#15651=CARTESIAN_POINT('',(-0.237175,-1.00305832390001E-14,12.6151410108095));
#15652=CARTESIAN_POINT('Ctrl Pts',(-0.237100373739744,0.000214889078547369,
13.2651410108095));
#15653=CARTESIAN_POINT('Ctrl Pts',(-0.23659111649862,-0.0575662489871676,
13.2690158822063));
#15654=CARTESIAN_POINT('Ctrl Pts',(-0.18624470561426,-0.195135369386986,
13.2781881494365));
#15655=CARTESIAN_POINT('Ctrl Pts',(0.0441614921479,-0.276932241019365,13.2926578125));
#15656=CARTESIAN_POINT('Ctrl Pts',(0.256726031781252,-0.1128425796642,13.30855));
#15657=CARTESIAN_POINT('Ctrl Pts',(0.233890236562906,0.154716040176168,
13.3244421875));
#15658=CARTESIAN_POINT('Ctrl Pts',(-0.00340698100913133,0.280410602722076,
13.340334375));
#15659=CARTESIAN_POINT('Ctrl Pts',(-0.20330767467579,0.168222136646133,
13.3539006494365));
#15660=CARTESIAN_POINT('Ctrl Pts',(-0.236686940146988,0.0443654745011182,
13.3621695280397));
#15661=CARTESIAN_POINT('Ctrl Pts',(-0.236817629449016,-7.78671831719799E-5,
13.3651410108095));
#15662=CARTESIAN_POINT('Ctrl Pts',(-0.236798662126443,-4.48389431123193E-5,
13.2848589891905));
#15663=CARTESIAN_POINT('Ctrl Pts',(-0.236860804307819,-0.0370025798760042,
13.2873295075623));
#15664=CARTESIAN_POINT('Ctrl Pts',(-0.211287036747699,-0.153238955594931,
13.2951050152614));
#15665=CARTESIAN_POINT('Ctrl Pts',(-0.0294466067184147,-0.279017272289624,
13.3081855122878));
#15666=CARTESIAN_POINT('Ctrl Pts',(0.218869047461476,-0.175539378629952,
13.3241004802698));
#15667=CARTESIAN_POINT('Ctrl Pts',(0.265969733682413,0.0893188257727471,
13.3400154482518));
#15668=CARTESIAN_POINT('Ctrl Pts',(0.0685537852907199,0.272062715339731,
13.3559304162339));
#15669=CARTESIAN_POINT('Ctrl Pts',(-0.176059774813894,0.208782676027031,
13.3708782632134));
#15670=CARTESIAN_POINT('Ctrl Pts',(-0.236717335476437,0.0643367149280847,
13.3805211208656));
#15671=CARTESIAN_POINT('Ctrl Pts',(-0.237306140600426,-0.000204717011637273,
13.3848589891905));
#15672=CARTESIAN_POINT('Origin',(0.,0.,12.6151410108095));
#15673=CARTESIAN_POINT('',(-0.237568867267691,-3.50085230488751E-5,13.1651410108095));
#15674=CARTESIAN_POINT('',(-0.23714100096821,0.000219260706363564,13.1848589891905));
#15675=CARTESIAN_POINT('',(-0.237175,-1.00305832390001E-14,12.6151410108095));
#15676=CARTESIAN_POINT('Ctrl Pts',(-0.237568867267691,-3.50085230488705E-5,
13.1651410108095));
#15677=CARTESIAN_POINT('Ctrl Pts',(-0.23757272817366,-0.00191072693511385,
13.1652674447063));
#15678=CARTESIAN_POINT('Ctrl Pts',(-0.236702342150314,-0.0823726342805651,
13.1706912744365));
#15679=CARTESIAN_POINT('Ctrl Pts',(-0.14620196384549,-0.239304592799359,
13.1814125));
#15680=CARTESIAN_POINT('Ctrl Pts',(0.12200497990914,-0.252500469855226,
13.1973046875));
#15681=CARTESIAN_POINT('Ctrl Pts',(0.278341649769444,-0.034170578184477,
13.213196875));
#15682=CARTESIAN_POINT('Ctrl Pts',(0.179457945287098,0.215491410897154,
13.2290890625));
#15683=CARTESIAN_POINT('Ctrl Pts',(-0.0839764970484053,0.267562423440159,
13.24498125));
#15684=CARTESIAN_POINT('Ctrl Pts',(-0.224953486042581,0.121419348905117,
13.2569985661032));
#15685=CARTESIAN_POINT('Ctrl Pts',(-0.237287329846353,0.0214272268439697,
13.263718486373));
#15686=CARTESIAN_POINT('Ctrl Pts',(-0.237100373739744,0.000214889078547369,
13.2651410108095));
#15687=CARTESIAN_POINT('Ctrl Pts',(-0.23714100096821,0.000219260706363571,
13.1848589891905));
#15688=CARTESIAN_POINT('Ctrl Pts',(-0.236601917095457,-0.0590126279016519,
13.1888329049316));
#15689=CARTESIAN_POINT('Ctrl Pts',(-0.184121441521327,-0.198168150201175,
13.19811181));
#15690=CARTESIAN_POINT('Ctrl Pts',(0.0497427765240963,-0.276122067797826,
13.2126957043958));
#15691=CARTESIAN_POINT('Ctrl Pts',(0.259221295320457,-0.107340859314887,
13.2286106723778));
#15692=CARTESIAN_POINT('Ctrl Pts',(0.23038737805747,0.160123065998856,13.2445256403598));
#15693=CARTESIAN_POINT('Ctrl Pts',(-0.0102508111899536,0.280379494845555,
13.2604406083418));
#15694=CARTESIAN_POINT('Ctrl Pts',(-0.205573087853117,0.164217542086628,
13.273885057952));
#15695=CARTESIAN_POINT('Ctrl Pts',(-0.236727365264118,0.0423574538123621,
13.2820245182349));
#15696=CARTESIAN_POINT('Ctrl Pts',(-0.236798662126443,-4.48389431123193E-5,
13.2848589891905));
#15697=CARTESIAN_POINT('Origin',(0.,0.,12.6151410108095));
#15698=CARTESIAN_POINT('',(-0.236996339228359,-0.000195082766924492,13.0651410108095));
#15699=CARTESIAN_POINT('',(-0.237565807314834,-4.77927823669955E-5,13.0848589891905));
#15700=CARTESIAN_POINT('',(-0.237175,-1.00305832390001E-14,12.6151410108095));
#15701=CARTESIAN_POINT('Ctrl Pts',(-0.236996339228359,-0.000195082766924502,
13.0651410108095));
#15702=CARTESIAN_POINT('Ctrl Pts',(-0.237189817656082,-0.0252059024681657,
13.0668164030397));
#15703=CARTESIAN_POINT('Ctrl Pts',(-0.222022384094442,-0.129069373509938,
13.0737891911032));
#15704=CARTESIAN_POINT('Ctrl Pts',(-0.0711327326516408,-0.271259720491414,
13.086059375));
#15705=CARTESIAN_POINT('Ctrl Pts',(0.189521520535091,-0.206696143611909,
13.1019515625));
#15706=CARTESIAN_POINT('Ctrl Pts',(0.276397422085156,0.0473937502037132,
13.11784375));
#15707=CARTESIAN_POINT('Ctrl Pts',(0.109835673593312,0.258026795320596,
13.1337359375));
#15708=CARTESIAN_POINT('Ctrl Pts',(-0.155311566263621,0.232273338104525,
13.1495016911032));
#15709=CARTESIAN_POINT('Ctrl Pts',(-0.237410961845922,0.0766791381988347,
13.159970048873));
#15710=CARTESIAN_POINT('Ctrl Pts',(-0.237568867267691,-3.50085230488705E-5,
13.1651410108095));
#15711=CARTESIAN_POINT('Ctrl Pts',(-0.237565807314834,-4.77927823669981E-5,
13.0848589891905));
#15712=CARTESIAN_POINT('Ctrl Pts',(-0.237572826099328,-0.0026043933601553,
13.0850313129736));
#15713=CARTESIAN_POINT('Ctrl Pts',(-0.236375116521228,-0.0838592301393141,
13.090508626084));
#15714=CARTESIAN_POINT('Ctrl Pts',(-0.143851548471854,-0.240882693501056,
13.1012909285217));
#15715=CARTESIAN_POINT('Ctrl Pts',(0.124964166840451,-0.25120051183695,
13.1172058965037));
#15716=CARTESIAN_POINT('Ctrl Pts',(0.278895358440525,-0.030579718254803,
13.1331208644857));
#15717=CARTESIAN_POINT('Ctrl Pts',(0.176426965387693,0.218154225247527,
13.1490358324677));
#15718=CARTESIAN_POINT('Ctrl Pts',(-0.0882377470317194,0.266330321450576,
13.1649508004497));
#15719=CARTESIAN_POINT('Ctrl Pts',(-0.225951591446148,0.118766717192262,
13.1768918526907));
#15720=CARTESIAN_POINT('Ctrl Pts',(-0.237321568536963,0.0200591384307359,
13.1835279156042));
#15721=CARTESIAN_POINT('Ctrl Pts',(-0.23714100096821,0.000219260706363571,
13.1848589891905));
#15722=CARTESIAN_POINT('Origin',(0.,0.,12.6151410108095));
#15723=CARTESIAN_POINT('',(-0.236868258229183,0.000132495174343476,12.9651410108095));
#15724=CARTESIAN_POINT('',(-0.236995674286161,-0.00019678875968307,12.9848589891905));
#15725=CARTESIAN_POINT('',(-0.237175,-1.00305832390001E-14,12.6151410108095));
#15726=CARTESIAN_POINT('Ctrl Pts',(-0.236868258229183,0.000132495174343491,
12.9651410108095));
#15727=CARTESIAN_POINT('Ctrl Pts',(-0.23662421943674,-0.0480671567343035,
12.968365361373));
#15728=CARTESIAN_POINT('Ctrl Pts',(-0.198883081137399,-0.175806934565607,
12.9768871077698));
#15729=CARTESIAN_POINT('Ctrl Pts',(0.00995747728231949,-0.28025434325381,
12.99070625));
#15730=CARTESIAN_POINT('Ctrl Pts',(0.240996248429915,-0.143396350591946,
13.0065984375));
#15731=CARTESIAN_POINT('Ctrl Pts',(0.251057922280563,0.124946521755194,
13.022490625));
#15732=CARTESIAN_POINT('Ctrl Pts',(0.0309165058329335,0.27872184254975,
13.0383828125));
#15733=CARTESIAN_POINT('Ctrl Pts',(-0.191376846905649,0.187659544819706,
13.0525996077698));
#15734=CARTESIAN_POINT('Ctrl Pts',(-0.236578061317235,0.0538754073814997,
13.0615190072063));
#15735=CARTESIAN_POINT('Ctrl Pts',(-0.236996339228359,-0.000195082766924502,
13.0651410108095));
#15736=CARTESIAN_POINT('Ctrl Pts',(-0.236995674286161,-0.000196788759683073,
12.9848589891905));
#15737=CARTESIAN_POINT('Ctrl Pts',(-0.237190390924988,-0.025212537514768,
12.9865347103429));
#15738=CARTESIAN_POINT('Ctrl Pts',(-0.222007629560777,-0.129192695194398,
12.9935154208226));
#15739=CARTESIAN_POINT('Ctrl Pts',(-0.0707617483345123,-0.271496792539298,
13.0058011206296));
#15740=CARTESIAN_POINT('Ctrl Pts',(0.19021711870995,-0.20624060859311,13.0217160886116));
#15741=CARTESIAN_POINT('Ctrl Pts',(0.276321843237659,0.0486207800379639,
13.0376310565936));
#15742=CARTESIAN_POINT('Ctrl Pts',(0.108392911780422,0.258783144727794,
13.0535460245757));
#15743=CARTESIAN_POINT('Ctrl Pts',(-0.156288642347958,0.231336327613849,
13.0692886687746));
#15744=CARTESIAN_POINT('Ctrl Pts',(-0.237356752750831,0.0761005801423566,
13.0797263236462));
#15745=CARTESIAN_POINT('Ctrl Pts',(-0.237565807314834,-4.77927823669981E-5,
13.0848589891905));
#15746=CARTESIAN_POINT('Origin',(0.,0.,12.6151410108095));
#15747=CARTESIAN_POINT('',(-0.237475867347687,0.000143668378376509,12.8651410108095));
#15748=CARTESIAN_POINT('',(-0.23685325391662,0.000124198907147655,12.8848589891905));
#15749=CARTESIAN_POINT('',(-0.237175,-1.00305832390001E-14,12.6151410108095));
#15750=CARTESIAN_POINT('Ctrl Pts',(-0.237475867347687,0.000143668378376506,
12.8651410108095));
#15751=CARTESIAN_POINT('Ctrl Pts',(-0.236995427452231,-0.0707374005589641,
12.8699143197063));
#15752=CARTESIAN_POINT('Ctrl Pts',(-0.165656267828233,-0.221154079023818,
12.8799850244365));
#15753=CARTESIAN_POINT('Ctrl Pts',(0.0902083908256771,-0.26551977706768,
12.895353125));
#15754=CARTESIAN_POINT('Ctrl Pts',(0.27207046341544,-0.0679625719645133,
12.9112453125));
#15755=CARTESIAN_POINT('Ctrl Pts',(0.204468796870817,0.191925109618724,
12.9271375));
#15756=CARTESIAN_POINT('Ctrl Pts',(-0.0506199491430696,0.275824015104995,
12.9430296875));
#15757=CARTESIAN_POINT('Ctrl Pts',(-0.216954845886699,0.141104430820563,
12.9556975244365));
#15758=CARTESIAN_POINT('Ctrl Pts',(-0.237025159116467,0.0311217001100208,
12.9630679655397));
#15759=CARTESIAN_POINT('Ctrl Pts',(-0.236868258229183,0.000132495174343491,
12.9651410108095));
#15760=CARTESIAN_POINT('Ctrl Pts',(-0.23685325391662,0.000124198907147644,
12.8848589891905));
#15761=CARTESIAN_POINT('Ctrl Pts',(-0.236630679274289,-0.0474065074335064,
12.8880381077122));
#15762=CARTESIAN_POINT('Ctrl Pts',(-0.199669376887335,-0.174571568479624,
12.8965222155612));
#15763=CARTESIAN_POINT('Ctrl Pts',(0.00797328488061451,-0.280452709922419,
12.9103113127376));
#15764=CARTESIAN_POINT('Ctrl Pts',(0.240296121102423,-0.14482920233622,
12.9262262807196));
#15765=CARTESIAN_POINT('Ctrl Pts',(0.251706166281744,0.123942967091746,
12.9421412487016));
#15766=CARTESIAN_POINT('Ctrl Pts',(0.0317122558575804,0.278768752799521,
12.9580562166836));
#15767=CARTESIAN_POINT('Ctrl Pts',(-0.191202431084563,0.187994314674536,
12.9722954635132));
#15768=CARTESIAN_POINT('Ctrl Pts',(-0.236573958000352,0.0539821900646985,
12.9812297210155));
#15769=CARTESIAN_POINT('Ctrl Pts',(-0.236995674286161,-0.000196788759683073,
12.9848589891905));
#15770=CARTESIAN_POINT('Origin',(0.,0.,13.55));
#15771=CARTESIAN_POINT('',(-0.286968182007205,0.000164849531348759,13.5133965297371));
#15772=CARTESIAN_POINT('Ctrl Pts',(-0.043944522199392,0.233068358199193,
13.562825));
#15773=CARTESIAN_POINT('Ctrl Pts',(-0.0294765840042651,0.236438793486496,
13.5621935878038));
#15774=CARTESIAN_POINT('Ctrl Pts',(-0.0147452085483875,0.238326827796529,
13.5615668352976));
#15775=CARTESIAN_POINT('Ctrl Pts',(6.08274638918418E-5,0.238832568630261,
13.560941941181));
#15776=CARTESIAN_POINT('Ctrl Pts',(0.00713427631766705,0.239074181707367,
13.5606434037083));
#15777=CARTESIAN_POINT('Ctrl Pts',(0.0142250285277132,0.2389995429081,13.5603452903877));
#15778=CARTESIAN_POINT('Ctrl Pts',(0.0213132083401427,0.238615554436029,
13.5600472957714));
#15779=CARTESIAN_POINT('Ctrl Pts',(0.0261835574655618,0.238351712664431,
13.5598425411155));
#15780=CARTESIAN_POINT('Ctrl Pts',(0.0310529721761364,0.237941454616689,
13.5596378302422));
#15781=CARTESIAN_POINT('Ctrl Pts',(0.0358999420287469,0.237388908068873,
13.5594336980816));
#15782=CARTESIAN_POINT('Ctrl Pts',(0.0493536867081515,0.235855203423731,
13.558867088003));
#15783=CARTESIAN_POINT('Ctrl Pts',(0.0626628489801356,0.23322660375155,
13.5583037466019));
#15784=CARTESIAN_POINT('Ctrl Pts',(0.0756903340245162,0.229556977452041,
13.5577416326332));
#15785=CARTESIAN_POINT('Ctrl Pts',(0.0818558888395591,0.227820242999976,
13.5574755993602));
#15786=CARTESIAN_POINT('Ctrl Pts',(0.087958354013132,0.225849872295259,
13.5572098410162));
#15787=CARTESIAN_POINT('Ctrl Pts',(0.0939827769363731,0.223649197682829,
13.5569441412149));
#15788=CARTESIAN_POINT('Ctrl Pts',(0.0979230858746843,0.222209833621548,
13.5567703587108));
#15789=CARTESIAN_POINT('Ctrl Pts',(0.101826955013135,0.220672876108273,
13.5565967330609));
#15790=CARTESIAN_POINT('Ctrl Pts',(0.105682387170434,0.219043149639582,
13.5564235627486));
#15791=CARTESIAN_POINT('Ctrl Pts',(0.119489970730244,0.21320655766286,13.5558033823229));
#15792=CARTESIAN_POINT('Ctrl Pts',(0.132707719562554,0.206172506490602,
13.5551876986953));
#15793=CARTESIAN_POINT('Ctrl Pts',(0.145152214688433,0.198000823300654,
13.5545738505959));
#15794=CARTESIAN_POINT('Ctrl Pts',(0.151794873917279,0.19363891820062,13.5542461889511));
#15795=CARTESIAN_POINT('Ctrl Pts',(0.158217051111106,0.188952135332664,
13.5539190502927));
#15796=CARTESIAN_POINT('Ctrl Pts',(0.164388452074525,0.183944806507876,
13.5535920298744));
#15797=CARTESIAN_POINT('Ctrl Pts',(0.168212225599151,0.180842287079498,
13.5533894094281));
#15798=CARTESIAN_POINT('Ctrl Pts',(0.171939685169454,0.17761664713226,13.553186834374));
#15799=CARTESIAN_POINT('Ctrl Pts',(0.175563092765558,0.174268326452765,
13.5529842084384));
#15800=CARTESIAN_POINT('Ctrl Pts',(0.177047466069561,0.172896645873624,
13.5529012002419));
#15801=CARTESIAN_POINT('Ctrl Pts',(0.178514082249302,0.171504603781964,
13.5528181987184));
#15802=CARTESIAN_POINT('Ctrl Pts',(0.179960409179589,0.170094285986212,
13.5527353145998));
#15803=CARTESIAN_POINT('Ctrl Pts',(0.190810527615469,0.159514302446048,
13.552113530905));
#15804=CARTESIAN_POINT('Ctrl Pts',(0.200553823179652,0.147879977988366,
13.5514965535525));
#15805=CARTESIAN_POINT('Ctrl Pts',(0.209172247663828,0.135414754877218,
13.5508817172788));
#15806=CARTESIAN_POINT('Ctrl Pts',(0.2150107423251,0.12697027193029,13.5504652005118));
#15807=CARTESIAN_POINT('Ctrl Pts',(0.220332398139305,0.118143361409001,
13.5500496663492));
#15808=CARTESIAN_POINT('Ctrl Pts',(0.225122317125784,0.108994362021549,
13.5496342861636));
#15809=CARTESIAN_POINT('Ctrl Pts',(0.227457000051293,0.104534993770087,
13.5494318232348));
#15810=CARTESIAN_POINT('Ctrl Pts',(0.229665233796247,0.0999990193216993,
13.5492293968869));
#15811=CARTESIAN_POINT('Ctrl Pts',(0.231744553284755,0.0953930457521194,
13.5490269111671));
#15812=CARTESIAN_POINT('Ctrl Pts',(0.233552950784709,0.0913872009869837,
13.5488508080375));
#15813=CARTESIAN_POINT('Ctrl Pts',(0.235260285198856,0.0873360923025083,
13.5486749987829));
#15814=CARTESIAN_POINT('Ctrl Pts',(0.236864416101865,0.083248529595993,
13.5484995890061));
#15815=CARTESIAN_POINT('Ctrl Pts',(0.242716576792444,0.0683363589330668,
13.547859662303));
#15816=CARTESIAN_POINT('Ctrl Pts',(0.247206036027669,0.0529249259443079,
13.5472243423549));
#15817=CARTESIAN_POINT('Ctrl Pts',(0.25028385037818,0.0372383602707011,
13.5465907037737));
#15818=CARTESIAN_POINT('Ctrl Pts',(0.252087300804334,0.0280467910832205,
13.5462194221955));
#15819=CARTESIAN_POINT('Ctrl Pts',(0.253405246706662,0.0187601746905643,
13.5458487178968));
#15820=CARTESIAN_POINT('Ctrl Pts',(0.254219891160352,0.00942114969984719,
13.5454780023471));
#15821=CARTESIAN_POINT('Ctrl Pts',(0.25478813976954,0.00290678881749256,
13.5452194127323));
#15822=CARTESIAN_POINT('Ctrl Pts',(0.255111030741479,-0.00363999231176376,
13.5449605458955));
#15823=CARTESIAN_POINT('Ctrl Pts',(0.255181476734096,-0.0101677045994756,
13.5447026610801));
#15824=CARTESIAN_POINT('Ctrl Pts',(0.255354370584029,-0.0261885067310612,
13.5440697407832));
#15825=CARTESIAN_POINT('Ctrl Pts',(0.254016166114596,-0.0421255321420965,
13.5434414744878));
#15826=CARTESIAN_POINT('Ctrl Pts',(0.251097893857644,-0.0577648854388578,
13.5428150415744));
#15827=CARTESIAN_POINT('Ctrl Pts',(0.250834755331568,-0.0591750747608081,
13.5427585565658));
#15828=CARTESIAN_POINT('Ctrl Pts',(0.250558734870263,-0.0605828459371271,
13.5427020864635));
#15829=CARTESIAN_POINT('Ctrl Pts',(0.250269760531176,-0.0619880420672277,
13.5426456291996));
#15830=CARTESIAN_POINT('Ctrl Pts',(0.248732768931078,-0.0694619743730475,
13.542345345304));
#15831=CARTESIAN_POINT('Ctrl Pts',(0.246829549128523,-0.0768631173570905,
13.5420454246012));
#15832=CARTESIAN_POINT('Ctrl Pts',(0.24457758894315,-0.0841750034805435,
13.5417455559504));
#15833=CARTESIAN_POINT('Ctrl Pts',(0.24320401817551,-0.0886348483306972,
13.5415626527109));
#15834=CARTESIAN_POINT('Ctrl Pts',(0.241700647647705,-0.0930614748590947,
13.5413797688365));
#15835=CARTESIAN_POINT('Ctrl Pts',(0.240070956053578,-0.0974509732874261,
13.5411968337233));
#15836=CARTESIAN_POINT('Ctrl Pts',(0.238427550824986,-0.101877408751667,
13.5410123592358));
#15837=CARTESIAN_POINT('Ctrl Pts',(0.236658304736593,-0.106258675580407,
13.5408281394574));
#15838=CARTESIAN_POINT('Ctrl Pts',(0.234770897270819,-0.110584625391991,
13.540644379461));
#15839=CARTESIAN_POINT('Ctrl Pts',(0.228360906593042,-0.125276364440202,
13.5400202959576));
#15840=CARTESIAN_POINT('Ctrl Pts',(0.220583153832133,-0.139355014290968,
13.5394005216076));
#15841=CARTESIAN_POINT('Ctrl Pts',(0.211608093803175,-0.15267492911545,
13.5387823454488));
#15842=CARTESIAN_POINT('Ctrl Pts',(0.205045157713066,-0.162415003213755,
13.5383303094057));
#15843=CARTESIAN_POINT('Ctrl Pts',(0.197840743027374,-0.171749337581638,
13.5378791279379));
#15844=CARTESIAN_POINT('Ctrl Pts',(0.190046593771134,-0.180613221027982,
13.5374277410453));
#15845=CARTESIAN_POINT('Ctrl Pts',(0.18689819700638,-0.184193730080112,
13.5372454061957));
#15846=CARTESIAN_POINT('Ctrl Pts',(0.183652322387751,-0.1876981824977,13.5370629859398));
#15847=CARTESIAN_POINT('Ctrl Pts',(0.180325161242096,-0.191109317049549,
13.5368811040816));
#15848=CARTESIAN_POINT('Ctrl Pts',(0.168744503055477,-0.202982256635035,
13.5362480383723));
#15849=CARTESIAN_POINT('Ctrl Pts',(0.156150610605738,-0.213764883234575,
13.5356196044284));
#15850=CARTESIAN_POINT('Ctrl Pts',(0.142703307452893,-0.223292717945068,
13.5349929842113));
#15851=CARTESIAN_POINT('Ctrl Pts',(0.13328997055946,-0.229962361439782,
13.5345543395892));
#15852=CARTESIAN_POINT('Ctrl Pts',(0.123457381914911,-0.236016716577223,
13.5341165837357));
#15853=CARTESIAN_POINT('Ctrl Pts',(0.113250289629505,-0.241387649069037,
13.5336787499942));
#15854=CARTESIAN_POINT('Ctrl Pts',(0.107437633034519,-0.244446246492947,
13.5334294157946));
#15855=CARTESIAN_POINT('Ctrl Pts',(0.101497232632265,-0.2472851876651,13.5331798094348));
#15856=CARTESIAN_POINT('Ctrl Pts',(0.0954700064811808,-0.249876992596412,
13.5329311101113));
#15857=CARTESIAN_POINT('Ctrl Pts',(0.0924351354571309,-0.251182036324465,
13.5328058832902));
#15858=CARTESIAN_POINT('Ctrl Pts',(0.0893771001161341,-0.252425149988217,
13.5326808351245));
#15859=CARTESIAN_POINT('Ctrl Pts',(0.0862971123270629,-0.253605021774803,
13.5325559437995));
#15860=CARTESIAN_POINT('Ctrl Pts',(0.071172071972524,-0.259399073442352,
13.5319426341176));
#15861=CARTESIAN_POINT('Ctrl Pts',(0.0555195588483159,-0.263672035534303,
13.5313331067171));
#15862=CARTESIAN_POINT('Ctrl Pts',(0.039552096653546,-0.266494984784699,
13.5307247782039));
#15863=CARTESIAN_POINT('Ctrl Pts',(0.028285188816394,-0.268486904893556,
13.5302955314514));
#15864=CARTESIAN_POINT('Ctrl Pts',(0.0168607381260563,-0.269755816583468,
13.5298668816188));
#15865=CARTESIAN_POINT('Ctrl Pts',(0.00534958536819863,-0.270312121070808,
13.5294379211004));
#15866=CARTESIAN_POINT('Ctrl Pts',(0.00115101094099197,-0.270515027403772,
13.5292814621688));
#15867=CARTESIAN_POINT('Ctrl Pts',(-0.00305507661402366,-0.270622704683305,
13.5291251120846));
#15868=CARTESIAN_POINT('Ctrl Pts',(-0.00725720002110199,-0.270636144905838,
13.5289691225271));
#15869=CARTESIAN_POINT('Ctrl Pts',(-0.0241769446018754,-0.270690261625018,
13.5283410344835));
#15870=CARTESIAN_POINT('Ctrl Pts',(-0.0410701020235392,-0.269222772099358,
13.5277173600727));
#15871=CARTESIAN_POINT('Ctrl Pts',(-0.057711020888307,-0.266291935802486,
13.5270953457536));
#15872=CARTESIAN_POINT('Ctrl Pts',(-0.0688902381852458,-0.264323026748199,
13.5266774822154));
#15873=CARTESIAN_POINT('Ctrl Pts',(-0.0799560150048115,-0.261692586303153,
13.5262603678815));
#15874=CARTESIAN_POINT('Ctrl Pts',(-0.0908391235420861,-0.258405107652052,
13.5258431679299));
#15875=CARTESIAN_POINT('Ctrl Pts',(-0.0950317449826877,-0.257138635537865,
13.5256824453334));
#15876=CARTESIAN_POINT('Ctrl Pts',(-0.0991994850387932,-0.25577373191658,
13.5255216219886));
#15877=CARTESIAN_POINT('Ctrl Pts',(-0.103330775485522,-0.254312914760898,
13.525360940178));
#15878=CARTESIAN_POINT('Ctrl Pts',(-0.119359411115515,-0.248645216928368,
13.5247375247519));
#15879=CARTESIAN_POINT('Ctrl Pts',(-0.134773006972199,-0.241563252903294,
13.5241188617021));
#15880=CARTESIAN_POINT('Ctrl Pts',(-0.149349294964951,-0.233107026334203,
13.5235022794556));
#15881=CARTESIAN_POINT('Ctrl Pts',(-0.157525060571445,-0.228363971972305,
13.5231564416176));
#15882=CARTESIAN_POINT('Ctrl Pts',(-0.165437317263121,-0.223187661340015,
13.5228112584068));
#15883=CARTESIAN_POINT('Ctrl Pts',(-0.17304417849703,-0.217578409204512,
13.5224662583993));
#15884=CARTESIAN_POINT('Ctrl Pts',(-0.17887039297022,-0.213282194909192,
13.5222020174758));
#15885=CARTESIAN_POINT('Ctrl Pts',(-0.184517406155673,-0.208731888546409,
13.5219378840244));
#15886=CARTESIAN_POINT('Ctrl Pts',(-0.189978938566547,-0.203943453156376,
13.521673646231));
#15887=CARTESIAN_POINT('Ctrl Pts',(-0.193403116199697,-0.200941282313685,
13.5215079789652));
#15888=CARTESIAN_POINT('Ctrl Pts',(-0.196754223511486,-0.197845265193714,
13.5213422693538));
#15889=CARTESIAN_POINT('Ctrl Pts',(-0.200020365596183,-0.194669931635478,
13.5211769999744));
#15890=CARTESIAN_POINT('Ctrl Pts',(-0.212036537758927,-0.182987845026729,
13.5205689721345));
#15891=CARTESIAN_POINT('Ctrl Pts',(-0.222942778207884,-0.170203637448647,
13.5199651042774));
#15892=CARTESIAN_POINT('Ctrl Pts',(-0.232682805209074,-0.156537147041984,
13.519362903645));
#15893=CARTESIAN_POINT('Ctrl Pts',(-0.241969469951098,-0.143506781254366,
13.5187887332263));
#15894=CARTESIAN_POINT('Ctrl Pts',(-0.250196294757052,-0.129672988479396,
13.5182160784383));
#15895=CARTESIAN_POINT('Ctrl Pts',(-0.257283810651443,-0.115198924292403,
13.5176427786581));
#15896=CARTESIAN_POINT('Ctrl Pts',(-0.259491932919989,-0.11068951592932,
13.5174641665704));
#15897=CARTESIAN_POINT('Ctrl Pts',(-0.261585787385611,-0.106124522483284,
13.5172857588748));
#15898=CARTESIAN_POINT('Ctrl Pts',(-0.263560449912049,-0.101516719136934,
13.5171077781986));
#15899=CARTESIAN_POINT('Ctrl Pts',(-0.270475851072545,-0.0853798814838883,
13.5164844778838));
#15900=CARTESIAN_POINT('Ctrl Pts',(-0.275946482637518,-0.0686925965880584,
13.5158653248676));
#15901=CARTESIAN_POINT('Ctrl Pts',(-0.279885783875338,-0.0516738313500138,
13.5152476263517));
#15902=CARTESIAN_POINT('Ctrl Pts',(-0.281958120038393,-0.0427208215332613,
13.5149226755812));
#15903=CARTESIAN_POINT('Ctrl Pts',(-0.283605922974178,-0.0336755953807322,
13.5145981273385));
#15904=CARTESIAN_POINT('Ctrl Pts',(-0.284810979317383,-0.0245681482391185,
13.5142735895868));
#15905=CARTESIAN_POINT('Ctrl Pts',(-0.285495319284535,-0.0193961161487672,
13.5140892877028));
#15906=CARTESIAN_POINT('Ctrl Pts',(-0.28603679820466,-0.014204004240413,
13.5139049892021));
#15907=CARTESIAN_POINT('Ctrl Pts',(-0.28643144246244,-0.00899727922140894,
13.5137206222854));
#15908=CARTESIAN_POINT('Ctrl Pts',(-0.286662860032101,-0.00594407972326887,
13.5136125103772));
#15909=CARTESIAN_POINT('Ctrl Pts',(-0.286843607970751,-0.00288741530408205,
13.5135044302464));
#15910=CARTESIAN_POINT('Ctrl Pts',(-0.28697292281753,0.000166992375313765,
13.5133965297371));
#15911=CARTESIAN_POINT('',(0.0261262957278421,0.292560460953161,13.5058));
#15912=CARTESIAN_POINT('Ctrl Pts',(0.0261206201035333,0.292499143797286,
13.5058));
#15913=CARTESIAN_POINT('Ctrl Pts',(0.00884643054260094,0.291825436047159,
13.5079854825731));
#15914=CARTESIAN_POINT('Ctrl Pts',(-0.00828334513464932,0.289706514159306,
13.5101847285682));
#15915=CARTESIAN_POINT('Ctrl Pts',(-0.0250574246257949,0.286137019621129,
13.5124084954842));
#15916=CARTESIAN_POINT('Ctrl Pts',(-0.0350258051457675,0.284015765823609,
13.5137300198526));
#15917=CARTESIAN_POINT('Ctrl Pts',(-0.0448683071666012,0.281381300825545,
13.5150602040358));
#15918=CARTESIAN_POINT('Ctrl Pts',(-0.0545358180860379,0.278224980453642,
13.5164013057481));
#15919=CARTESIAN_POINT('Ctrl Pts',(-0.0606603459790604,0.27622539934966,
13.5172509158404));
#15920=CARTESIAN_POINT('Ctrl Pts',(-0.0667145579989015,0.274016266063491,
13.5181049076087));
#15921=CARTESIAN_POINT('Ctrl Pts',(-0.072684837684636,0.27159431964496,
13.5189638550939));
#15922=CARTESIAN_POINT('Ctrl Pts',(-0.0764355024604301,0.270072798108449,
13.5195034653377));
#15923=CARTESIAN_POINT('Ctrl Pts',(-0.0801508179192932,0.268468026109448,
13.520044724687));
#15924=CARTESIAN_POINT('Ctrl Pts',(-0.0838198221478387,0.266783197590374,
13.5205866293988));
#15925=CARTESIAN_POINT('Ctrl Pts',(-0.0942230095561321,0.262005992184504,
13.5221231597279));
#15926=CARTESIAN_POINT('Ctrl Pts',(-0.104273334180971,0.256578412344035,
13.5236675754247));
#15927=CARTESIAN_POINT('Ctrl Pts',(-0.113901775440171,0.250492155939794,
13.5252236806533));
#15928=CARTESIAN_POINT('Ctrl Pts',(-0.126477796119793,0.242542698250774,
13.5272561603671));
#15929=CARTESIAN_POINT('Ctrl Pts',(-0.138335359995195,0.233469464109384,
13.5293085822151));
#15930=CARTESIAN_POINT('Ctrl Pts',(-0.149379447945921,0.223405603100387,
13.5313894227842));
#15931=CARTESIAN_POINT('Ctrl Pts',(-0.153219453627113,0.219906420223386,
13.5321129265848));
#15932=CARTESIAN_POINT('Ctrl Pts',(-0.156960833903308,0.216287355644465,
13.5328398660326));
#15933=CARTESIAN_POINT('Ctrl Pts',(-0.160598645982812,0.212553746141513,
13.5335705974367));
#15934=CARTESIAN_POINT('Ctrl Pts',(-0.163567294871897,0.209506921440021,
13.534166913278));
#15935=CARTESIAN_POINT('Ctrl Pts',(-0.166463512525863,0.2063871883392,13.5347650814277));
#15936=CARTESIAN_POINT('Ctrl Pts',(-0.169280235000242,0.203203670539578,
13.5353642364953));
#15937=CARTESIAN_POINT('Ctrl Pts',(-0.179529104895811,0.191620186531006,
13.5375443101058));
#15938=CARTESIAN_POINT('Ctrl Pts',(-0.188750918175532,0.179170970598589,
13.5397418585162));
#15939=CARTESIAN_POINT('Ctrl Pts',(-0.196842895670712,0.166013931025591,
13.5419679679277));
#15940=CARTESIAN_POINT('Ctrl Pts',(-0.203730824185022,0.154814598341739,
13.543862842512));
#15941=CARTESIAN_POINT('Ctrl Pts',(-0.209799618039609,0.143101506632859,
13.5457784109491));
#15942=CARTESIAN_POINT('Ctrl Pts',(-0.214959055570843,0.130969922145647,
13.5477215105393));
#15943=CARTESIAN_POINT('Ctrl Pts',(-0.216612406033525,0.127082335426442,
13.5483441800816));
#15944=CARTESIAN_POINT('Ctrl Pts',(-0.218171913124406,0.123151835124804,
13.5489696646219));
#15945=CARTESIAN_POINT('Ctrl Pts',(-0.219629934580908,0.11919478632138,
13.549596137626));
#15946=CARTESIAN_POINT('Ctrl Pts',(-0.224740451337889,0.105324918955647,
13.551791990623));
#15947=CARTESIAN_POINT('Ctrl Pts',(-0.228625673283085,0.0910885104257726,
13.5540064494166));
#15948=CARTESIAN_POINT('Ctrl Pts',(-0.231173355347657,0.0766269568750346,
13.5562511496559));
#15949=CARTESIAN_POINT('Ctrl Pts',(-0.233624712277369,0.0627121792016433,
13.5584109801792));
#15950=CARTESIAN_POINT('Ctrl Pts',(-0.234837706655883,0.0485878801050229,
13.5605988085852));
#15951=CARTESIAN_POINT('Ctrl Pts',(-0.234668236863856,0.0343918483395283,
13.562825));
#15952=CARTESIAN_POINT('',(-0.214330452128339,0.201110949933342,13.5058));
#15953=CARTESIAN_POINT('Origin',(0.,0.,13.5058));
#15954=CARTESIAN_POINT('Ctrl Pts',(-0.28697292281753,0.000166992375313765,
13.5133965297371));
#15955=CARTESIAN_POINT('Ctrl Pts',(-0.287381793203279,0.00982448242552759,
13.513055367651));
#15956=CARTESIAN_POINT('Ctrl Pts',(-0.287277908684719,0.0194726610186102,
13.512715528512));
#15957=CARTESIAN_POINT('Ctrl Pts',(-0.286645660444495,0.0290760529402092,
13.5123765729991));
#15958=CARTESIAN_POINT('Ctrl Pts',(-0.285612853120713,0.0447636466395815,
13.5118228731802));
#15959=CARTESIAN_POINT('Ctrl Pts',(-0.283172279973397,0.0603320811344235,
13.5112715312968));
#15960=CARTESIAN_POINT('Ctrl Pts',(-0.279438676347389,0.0756505557756192,
13.5107206323131));
#15961=CARTESIAN_POINT('Ctrl Pts',(-0.277817724983914,0.082301101694054,
13.510481458435));
#15962=CARTESIAN_POINT('Ctrl Pts',(-0.275952566041092,0.0889045063031122,
13.5102423680381));
#15963=CARTESIAN_POINT('Ctrl Pts',(-0.27385050370512,0.0954496671937427,
13.5100032044105));
#15964=CARTESIAN_POINT('Ctrl Pts',(-0.272052647080838,0.101047627188955,
13.5097986520026));
#15965=CARTESIAN_POINT('Ctrl Pts',(-0.270079941233438,0.106606043452002,
13.5095939285241));
#15966=CARTESIAN_POINT('Ctrl Pts',(-0.267946682411625,0.112093614932915,
13.5093898414744));
#15967=CARTESIAN_POINT('Ctrl Pts',(-0.261495892531522,0.128687555721275,
13.5087726999153));
#15968=CARTESIAN_POINT('Ctrl Pts',(-0.253568602001536,0.144679477818713,
13.5081597540965));
#15969=CARTESIAN_POINT('Ctrl Pts',(-0.244320225481875,0.159886712194555,
13.50754839969));
#15970=CARTESIAN_POINT('Ctrl Pts',(-0.235493300050023,0.174400948674316,
13.5069649048737));
#15971=CARTESIAN_POINT('Ctrl Pts',(-0.225461890301029,0.188201490936452,
13.5063828597325));
#15972=CARTESIAN_POINT('Ctrl Pts',(-0.214321504642966,0.201109806014094,
13.5058));
#15973=CARTESIAN_POINT('',(-0.199999999999999,-2.4492935982947E-17,13.6));
#15974=CARTESIAN_POINT('',(-0.25,-3.06161699786838E-17,13.55));
#15975=CARTESIAN_POINT('Origin',(0.,0.,13.6));
#15976=CARTESIAN_POINT('Ctrl Pts',(0.170810875200406,-0.23953556085323,
12.7670766008995));
#15977=CARTESIAN_POINT('Ctrl Pts',(0.250539136060416,-0.182681981504947,
12.7723739967328));
#15978=CARTESIAN_POINT('Ctrl Pts',(0.347291359551364,0.0160604774249761,
12.7829687883995));
#15979=CARTESIAN_POINT('Ctrl Pts',(0.174450423592672,0.301171722453608,
12.7988609758995));
#15980=CARTESIAN_POINT('Ctrl Pts',(-0.158655251249622,0.309505572481922,
12.8147531633995));
#15981=CARTESIAN_POINT('Ctrl Pts',(-0.346141364686362,0.0343485950558648,
12.8306453508995));
#15982=CARTESIAN_POINT('Ctrl Pts',(-0.216309200137717,-0.272450359979308,
12.8465375383995));
#15983=CARTESIAN_POINT('Ctrl Pts',(0.111897580187261,-0.329359833090805,
12.8624297258995));
#15984=CARTESIAN_POINT('Ctrl Pts',(0.337485528984177,-0.0843031039188804,
12.8783219133995));
#15985=CARTESIAN_POINT('Ctrl Pts',(0.253630104519426,0.238070484873314,
12.8942141008995));
#15986=CARTESIAN_POINT('Ctrl Pts',(-0.0627907200922966,0.342141563165973,
12.9101062883995));
#15987=CARTESIAN_POINT('Ctrl Pts',(-0.321634866420445,0.132495983852973,
12.9259984758995));
#15988=CARTESIAN_POINT('Ctrl Pts',(-0.285562599947175,-0.198641295410301,
12.9418906633995));
#15989=CARTESIAN_POINT('Ctrl Pts',(0.0123515961482354,-0.347637094066705,
12.9577828508995));
#15990=CARTESIAN_POINT('Ctrl Pts',(0.298940007539078,-0.177873748684098,
12.9736750383995));
#15991=CARTESIAN_POINT('Ctrl Pts',(0.311420852682373,0.15498794856278,12.9895672258995));
#15992=CARTESIAN_POINT('Ctrl Pts',(0.0383498936061967,0.345736127661585,
13.0054594133994));
#15993=CARTESIAN_POINT('Ctrl Pts',(-0.269885287401924,0.219467827336637,
13.0213516008995));
#15994=CARTESIAN_POINT('Ctrl Pts',(-0.330654015328618,-0.108037577904655,
13.0372437883995));
#15995=CARTESIAN_POINT('Ctrl Pts',(-0.0882354799035033,-0.336479855670175,
13.0531359758995));
#15996=CARTESIAN_POINT('Ctrl Pts',(0.235088990582579,-0.256392981767151,
13.0690281633995));
#15997=CARTESIAN_POINT('Ctrl Pts',(0.342852836839687,0.0587888323387024,
13.0849203508995));
#15998=CARTESIAN_POINT('Ctrl Pts',(0.136243934525784,0.320065281683648,
13.1008125383995));
#15999=CARTESIAN_POINT('Ctrl Pts',(-0.195291395037498,0.287863622974583,
13.1167047258995));
#16000=CARTESIAN_POINT('Ctrl Pts',(-0.347757789320859,-0.00828941245669413,
13.1325969133995));
#16001=CARTESIAN_POINT('Ctrl Pts',(-0.18135392753597,-0.296841619907541,
13.1484891008995));
#16002=CARTESIAN_POINT('Ctrl Pts',(0.151339159225333,-0.313210238142333,
13.1643812883995));
#16003=CARTESIAN_POINT('Ctrl Pts',(0.34526452350446,-0.0423863564957258,
13.1802734758995));
#16004=CARTESIAN_POINT('Ctrl Pts',(0.222605786880847,0.267302932796215,
13.1961656633995));
#16005=CARTESIAN_POINT('Ctrl Pts',(-0.104167325526047,0.331893601670054,
13.2120578508995));
#16006=CARTESIAN_POINT('Ctrl Pts',(-0.335426081500374,0.0921603951917061,
13.2279500383995));
#16007=CARTESIAN_POINT('Ctrl Pts',(-0.259121917540537,-0.232077627176206,
13.2438422258995));
#16008=CARTESIAN_POINT('Ctrl Pts',(0.0547794286493582,-0.343516244578465,
13.2597344133995));
#16009=CARTESIAN_POINT('Ctrl Pts',(0.31845177000124,-0.139973803888303,
13.2756266008995));
#16010=CARTESIAN_POINT('Ctrl Pts',(0.290125466835911,0.191915079666188,
13.2915187883995));
#16011=CARTESIAN_POINT('Ctrl Pts',(-0.00422613602987575,0.34783092366748,
13.3074109758995));
#16012=CARTESIAN_POINT('Ctrl Pts',(-0.294702729176935,0.1848093612187,13.3233031633995));
#16013=CARTESIAN_POINT('Ctrl Pts',(-0.314956806266814,-0.147669635622091,
13.3391953508995));
#16014=CARTESIAN_POINT('Ctrl Pts',(-0.0464171970913749,-0.344746002942823,
13.3550875383995));
#16015=CARTESIAN_POINT('Ctrl Pts',(0.264684441815691,-0.225712913443562,
13.3709797258995));
#16016=CARTESIAN_POINT('Ctrl Pts',(0.333087167753441,0.100281914886762,
13.3868719133995));
#16017=CARTESIAN_POINT('Ctrl Pts',(0.0960742243350252,0.334328474863828,
13.4027641008994));
#16018=CARTESIAN_POINT('Ctrl Pts',(-0.229037672424893,0.261811459287546,
13.4186562883995));
#16019=CARTESIAN_POINT('Ctrl Pts',(-0.344126396035303,-0.0507542279728567,
13.4345484758994));
#16020=CARTESIAN_POINT('Ctrl Pts',(-0.143697728706779,-0.316811981278465,
13.4504406633995));
#16021=CARTESIAN_POINT('Ctrl Pts',(0.188539763103792,-0.292312209902382,
13.4663328508995));
#16022=CARTESIAN_POINT('Ctrl Pts',(0.347800489128543,8.89291240029669E-5,
13.4822250383995));
#16023=CARTESIAN_POINT('Ctrl Pts',(0.188357478725655,0.292675275528102,
13.4981172258995));
#16024=CARTESIAN_POINT('Ctrl Pts',(-0.144211765716315,0.316341894132181,
13.5140094133995));
#16025=CARTESIAN_POINT('Ctrl Pts',(-0.276891073531918,0.139548910647182,
13.5246042050661));
#16026=CARTESIAN_POINT('Ctrl Pts',(-0.291090525077881,0.0426608275808572,
13.5299016008995));
#16027=CARTESIAN_POINT('Ctrl Pts',(0.159774743137974,-0.224059110187407,
12.7780510672663));
#16028=CARTESIAN_POINT('Ctrl Pts',(0.23435174173247,-0.170878854385844,
12.7833484630996));
#16029=CARTESIAN_POINT('Ctrl Pts',(0.324852780604597,0.0150228060844386,
12.7939432547663));
#16030=CARTESIAN_POINT('Ctrl Pts',(0.163179139426149,0.281712944442145,
12.8098354422663));
#16031=CARTESIAN_POINT('Ctrl Pts',(-0.148404496997968,0.289508342399459,
12.8257276297663));
#16032=CARTESIAN_POINT('Ctrl Pts',(-0.323777087186656,0.0321293240009572,
12.8416198172663));
#16033=CARTESIAN_POINT('Ctrl Pts',(-0.202333410269313,-0.254847276161248,
12.8575120047663));
#16034=CARTESIAN_POINT('Ctrl Pts',(0.104667850400066,-0.308079814416429,
12.8734041922663));
#16035=CARTESIAN_POINT('Ctrl Pts',(0.315680507127931,-0.0788562599340915,
12.8892963797663));
#16036=CARTESIAN_POINT('Ctrl Pts',(0.23724300196989,0.222688693121784,12.9051885672663));
#16037=CARTESIAN_POINT('Ctrl Pts',(-0.0587337964425541,0.320035713812314,
12.9210807547663));
#16038=CARTESIAN_POINT('Ctrl Pts',(-0.30085395971568,0.123935386210534,
12.9369729422663));
#16039=CARTESIAN_POINT('Ctrl Pts',(-0.267112331125525,-0.185807033150192,
12.9528651297663));
#16040=CARTESIAN_POINT('Ctrl Pts',(0.0115535565262634,-0.325176177129073,
12.9687573172663));
#16041=CARTESIAN_POINT('Ctrl Pts',(0.279625421169357,-0.166381282653381,
12.9846495047663));
#16042=CARTESIAN_POINT('Ctrl Pts',(0.29129987588177,0.144974139626918,13.0005416922663));
#16043=CARTESIAN_POINT('Ctrl Pts',(0.0358720976817757,0.323398032624307,
13.0164338797663));
#16044=CARTESIAN_POINT('Ctrl Pts',(-0.252447933545031,0.205287957799053,
13.0323260672663));
#16045=CARTESIAN_POINT('Ctrl Pts',(-0.309290379226063,-0.101057243800857,
13.0482182547663));
#16046=CARTESIAN_POINT('Ctrl Pts',(-0.0825345641528824,-0.314739810610588,
13.0641104422663));
#16047=CARTESIAN_POINT('Ctrl Pts',(0.219899833900083,-0.239827369048737,
13.0800026297663));
#16048=CARTESIAN_POINT('Ctrl Pts',(0.32070103192151,0.0549904716270394,
13.0958948172663));
#16049=CARTESIAN_POINT('Ctrl Pts',(0.127441180881627,0.299385786229297,
13.1117870047663));
#16050=CARTESIAN_POINT('Ctrl Pts',(-0.182673570652711,0.269264684497214,
13.1276791922663));
#16051=CARTESIAN_POINT('Ctrl Pts',(-0.325289074233592,-0.00775383150797187,
13.1435713797663));
#16052=CARTESIAN_POINT('Ctrl Pts',(-0.16963660630581,-0.27766261087148,
13.1594635672663));
#16053=CARTESIAN_POINT('Ctrl Pts',(0.141561099453268,-0.292973648713298,
13.1753557547663));
#16054=CARTESIAN_POINT('Ctrl Pts',(0.322956898926121,-0.0396477637253095,
13.1912479422663));
#16055=CARTESIAN_POINT('Ctrl Pts',(0.208223173016264,0.250032425496528,
13.2071401297663));
#16056=CARTESIAN_POINT('Ctrl Pts',(-0.0974370493668332,0.310449875593422,
13.2230323172663));
#16057=CARTESIAN_POINT('Ctrl Pts',(-0.313754121045401,0.0862058897126582,
13.2389245047663));
#16058=CARTESIAN_POINT('Ctrl Pts',(-0.242379987620132,-0.217083035413547,
13.2548166922663));
#16059=CARTESIAN_POINT('Ctrl Pts',(0.0512401164822056,-0.321321576725432,
13.2707088797663));
#16060=CARTESIAN_POINT('Ctrl Pts',(0.29787652392791,-0.130930062480268,
13.2866010672663));
#16061=CARTESIAN_POINT('Ctrl Pts',(0.271380390078243,0.179515399836181,
13.3024932547663));
#16062=CARTESIAN_POINT('Ctrl Pts',(-0.00395308435629426,0.325357483352345,
13.3183854422663));
#16063=CARTESIAN_POINT('Ctrl Pts',(-0.275661914389586,0.172868783580475,
13.3342776297663));
#16064=CARTESIAN_POINT('Ctrl Pts',(-0.294607370647773,-0.138128664659764,
13.3501698172663));
#16065=CARTESIAN_POINT('Ctrl Pts',(-0.0434181707327341,-0.322471880103695,
13.3660620047663));
#16066=CARTESIAN_POINT('Ctrl Pts',(0.247583115853149,-0.211129547378391,
13.3819541922663));
#16067=CARTESIAN_POINT('Ctrl Pts',(0.311566325082764,0.0938026760510299,
13.3978463797663));
#16068=CARTESIAN_POINT('Ctrl Pts',(0.0898668454060592,0.312727431039774,
13.4137385672663));
#16069=CARTESIAN_POINT('Ctrl Pts',(-0.214239492875801,0.244895757422746,
13.4296307547663));
#16070=CARTESIAN_POINT('Ctrl Pts',(-0.321892306148703,-0.0474749849973848,
13.4455229422663));
#16071=CARTESIAN_POINT('Ctrl Pts',(-0.1344133836133,-0.296342682352107,
13.4614151297663));
#16072=CARTESIAN_POINT('Ctrl Pts',(0.17635816329528,-0.273425847144979,
13.4773073172663));
#16073=CARTESIAN_POINT('Ctrl Pts',(0.325329015196348,8.31833917395924E-5,
13.4931995047663));
#16074=CARTESIAN_POINT('Ctrl Pts',(0.17618765635501,0.273765455012591,13.5090916922663));
#16075=CARTESIAN_POINT('Ctrl Pts',(-0.134894208567015,0.295902967650323,
13.5249838797663));
#16076=CARTESIAN_POINT('Ctrl Pts',(-0.259001074134504,0.130532621694478,
13.535578671433));
#16077=CARTESIAN_POINT('Ctrl Pts',(-0.272283095673206,0.0399045011670809,
13.5408760672663));
#16078=CARTESIAN_POINT('Ctrl Pts',(0.148738611075541,-0.208582659521583,
12.7890255336332));
#16079=CARTESIAN_POINT('Ctrl Pts',(0.218164347404524,-0.159075727266742,
12.7943229294665));
#16080=CARTESIAN_POINT('Ctrl Pts',(0.30241420165783,0.0139851347439006,
12.8049177211332));
#16081=CARTESIAN_POINT('Ctrl Pts',(0.151907855259627,0.262254166430683,
12.8208099086331));
#16082=CARTESIAN_POINT('Ctrl Pts',(-0.138153742746315,0.269511112316996,
12.8367020961332));
#16083=CARTESIAN_POINT('Ctrl Pts',(-0.301412809686951,0.0299100529460499,
12.8525942836332));
#16084=CARTESIAN_POINT('Ctrl Pts',(-0.188357620400908,-0.237244192343189,
12.8684864711332));
#16085=CARTESIAN_POINT('Ctrl Pts',(0.0974381206128715,-0.286799795742055,
12.8843786586331));
#16086=CARTESIAN_POINT('Ctrl Pts',(0.293875485271686,-0.0734094159493023,
12.9002708461332));
#16087=CARTESIAN_POINT('Ctrl Pts',(0.220855899420353,0.207306901370254,
12.9161630336331));
#16088=CARTESIAN_POINT('Ctrl Pts',(-0.0546768727928118,0.297929864458655,
12.9320552211332));
#16089=CARTESIAN_POINT('Ctrl Pts',(-0.280073053010915,0.115374788568095,
12.9479474086332));
#16090=CARTESIAN_POINT('Ctrl Pts',(-0.248662062303876,-0.172972770890084,
12.9638395961331));
#16091=CARTESIAN_POINT('Ctrl Pts',(0.0107555169042914,-0.302715260191442,
12.9797317836332));
#16092=CARTESIAN_POINT('Ctrl Pts',(0.260310834799636,-0.154888816622663,
12.9956239711332));
#16093=CARTESIAN_POINT('Ctrl Pts',(0.271178899081166,0.134960330691056,
13.0115161586332));
#16094=CARTESIAN_POINT('Ctrl Pts',(0.0333943017573545,0.301059937587029,
13.0274083461332));
#16095=CARTESIAN_POINT('Ctrl Pts',(-0.235010579688137,0.191108088261468,
13.0433005336332));
#16096=CARTESIAN_POINT('Ctrl Pts',(-0.287926743123509,-0.0940769096970587,
13.0591927211332));
#16097=CARTESIAN_POINT('Ctrl Pts',(-0.0768336484022617,-0.292999765551001,
13.0750849086331));
#16098=CARTESIAN_POINT('Ctrl Pts',(0.204710677217587,-0.223261756330323,
13.0909770961332));
#16099=CARTESIAN_POINT('Ctrl Pts',(0.298549227003333,0.0511921109153762,
13.1068692836332));
#16100=CARTESIAN_POINT('Ctrl Pts',(0.118638427237469,0.278706290774946,
13.1227614711331));
#16101=CARTESIAN_POINT('Ctrl Pts',(-0.170055746267924,0.250665746019845,
13.1386536586332));
#16102=CARTESIAN_POINT('Ctrl Pts',(-0.302820359146324,-0.00721825055924952,
13.1545458461331));
#16103=CARTESIAN_POINT('Ctrl Pts',(-0.15791928507565,-0.258483601835419,
13.1704380336332));
#16104=CARTESIAN_POINT('Ctrl Pts',(0.131783039681204,-0.272737059284262,
13.1863302211331));
#16105=CARTESIAN_POINT('Ctrl Pts',(0.300649274347783,-0.0369091709548933,
13.2022224086332));
#16106=CARTESIAN_POINT('Ctrl Pts',(0.193840559151681,0.232761918196841,
13.2181145961331));
#16107=CARTESIAN_POINT('Ctrl Pts',(-0.0907067732076193,0.289006149516791,
13.2340067836332));
#16108=CARTESIAN_POINT('Ctrl Pts',(-0.292082160590429,0.0802513842336103,
13.2498989711331));
#16109=CARTESIAN_POINT('Ctrl Pts',(-0.225638057699727,-0.202088443650888,
13.2657911586332));
#16110=CARTESIAN_POINT('Ctrl Pts',(0.0477008043150527,-0.299126908872399,
13.2816833461332));
#16111=CARTESIAN_POINT('Ctrl Pts',(0.277301277854581,-0.121886321072234,
13.2975755336331));
#16112=CARTESIAN_POINT('Ctrl Pts',(0.252635313320574,0.167115720006175,
13.3134677211332));
#16113=CARTESIAN_POINT('Ctrl Pts',(-0.00368003268271287,0.302884043037211,
13.3293599086331));
#16114=CARTESIAN_POINT('Ctrl Pts',(-0.256621099602237,0.160928205942251,
13.3452520961332));
#16115=CARTESIAN_POINT('Ctrl Pts',(-0.274257935028732,-0.128587693697438,
13.3611442836331));
#16116=CARTESIAN_POINT('Ctrl Pts',(-0.0404191443740934,-0.300197757264567,
13.3770364711332));
#16117=CARTESIAN_POINT('Ctrl Pts',(0.230481789890607,-0.196546181313221,
13.3929286586331));
#16118=CARTESIAN_POINT('Ctrl Pts',(0.290045482412086,0.0873234372152981,
13.4088208461332));
#16119=CARTESIAN_POINT('Ctrl Pts',(0.0836594664770931,0.291126387215721,
13.4247130336331));
#16120=CARTESIAN_POINT('Ctrl Pts',(-0.199441313326708,0.227980055557946,
13.4406052211332));
#16121=CARTESIAN_POINT('Ctrl Pts',(-0.299658216262103,-0.044195742021913,
13.4564974086332));
#16122=CARTESIAN_POINT('Ctrl Pts',(-0.125129038519821,-0.275873383425748,
13.4723895961332));
#16123=CARTESIAN_POINT('Ctrl Pts',(0.164176563486767,-0.254539484387576,
13.4882817836332));
#16124=CARTESIAN_POINT('Ctrl Pts',(0.302857541264153,7.7437659476318E-5,
13.5041739711332));
#16125=CARTESIAN_POINT('Ctrl Pts',(0.164017833984366,0.25485563449708,13.5200661586332));
#16126=CARTESIAN_POINT('Ctrl Pts',(-0.125576651417715,0.275464041168465,
13.5359583461332));
#16127=CARTESIAN_POINT('Ctrl Pts',(-0.241111074737091,0.121516332741775,
13.5465531377998));
#16128=CARTESIAN_POINT('Ctrl Pts',(-0.253475666268531,0.0371481747533046,
13.5518505336332));
#16129=CARTESIAN_POINT('Ctrl Pts',(0.137702479013109,-0.19310620885576,
12.8));
#16130=CARTESIAN_POINT('Ctrl Pts',(0.201976953076579,-0.147272600147639,
12.8052973958333));
#16131=CARTESIAN_POINT('Ctrl Pts',(0.279975622711063,0.012947463403363,
12.8158921875));
#16132=CARTESIAN_POINT('Ctrl Pts',(0.140636571093104,0.242795388419221,
12.831784375));
#16133=CARTESIAN_POINT('Ctrl Pts',(-0.127902988494662,0.249513882234533,
12.8476765625));
#16134=CARTESIAN_POINT('Ctrl Pts',(-0.279048532187246,0.0276907818911422,
12.86356875));
#16135=CARTESIAN_POINT('Ctrl Pts',(-0.174381830532504,-0.219641108525129,
12.8794609375));
#16136=CARTESIAN_POINT('Ctrl Pts',(0.0902083908256771,-0.26551977706768,
12.895353125));
#16137=CARTESIAN_POINT('Ctrl Pts',(0.27207046341544,-0.0679625719645133,
12.9112453125));
#16138=CARTESIAN_POINT('Ctrl Pts',(0.204468796870817,0.191925109618724,
12.9271375));
#16139=CARTESIAN_POINT('Ctrl Pts',(-0.0506199491430696,0.275824015104995,
12.9430296875));
#16140=CARTESIAN_POINT('Ctrl Pts',(-0.25929214630615,0.106814190925657,
12.958921875));
#16141=CARTESIAN_POINT('Ctrl Pts',(-0.230211793482226,-0.160138508629975,
12.9748140625));
#16142=CARTESIAN_POINT('Ctrl Pts',(0.00995747728231949,-0.28025434325381,
12.99070625));
#16143=CARTESIAN_POINT('Ctrl Pts',(0.240996248429915,-0.143396350591946,
13.0065984375));
#16144=CARTESIAN_POINT('Ctrl Pts',(0.251057922280563,0.124946521755194,
13.022490625));
#16145=CARTESIAN_POINT('Ctrl Pts',(0.0309165058329335,0.27872184254975,
13.0383828125));
#16146=CARTESIAN_POINT('Ctrl Pts',(-0.217573225831243,0.176928218723883,
13.054275));
#16147=CARTESIAN_POINT('Ctrl Pts',(-0.266563107020954,-0.0870965755932605,
13.0701671875));
#16148=CARTESIAN_POINT('Ctrl Pts',(-0.0711327326516408,-0.271259720491414,
13.086059375));
#16149=CARTESIAN_POINT('Ctrl Pts',(0.189521520535091,-0.206696143611909,
13.1019515625));
#16150=CARTESIAN_POINT('Ctrl Pts',(0.276397422085156,0.0473937502037132,
13.11784375));
#16151=CARTESIAN_POINT('Ctrl Pts',(0.109835673593312,0.258026795320596,
13.1337359375));
#16152=CARTESIAN_POINT('Ctrl Pts',(-0.157437921883138,0.232066807542476,
13.149628125));
#16153=CARTESIAN_POINT('Ctrl Pts',(-0.280351644059057,-0.00668266961052725,
13.1655203125));
#16154=CARTESIAN_POINT('Ctrl Pts',(-0.14620196384549,-0.239304592799359,
13.1814125));
#16155=CARTESIAN_POINT('Ctrl Pts',(0.12200497990914,-0.252500469855226,
13.1973046875));
#16156=CARTESIAN_POINT('Ctrl Pts',(0.278341649769444,-0.034170578184477,
13.213196875));
#16157=CARTESIAN_POINT('Ctrl Pts',(0.179457945287098,0.215491410897154,
13.2290890625));
#16158=CARTESIAN_POINT('Ctrl Pts',(-0.0839764970484053,0.267562423440159,
13.24498125));
#16159=CARTESIAN_POINT('Ctrl Pts',(-0.270410200135457,0.0742968787545624,
13.2608734375));
#16160=CARTESIAN_POINT('Ctrl Pts',(-0.208896127779322,-0.18709385188823,
13.276765625));
#16161=CARTESIAN_POINT('Ctrl Pts',(0.0441614921479,-0.276932241019365,13.2926578125));
#16162=CARTESIAN_POINT('Ctrl Pts',(0.256726031781252,-0.1128425796642,13.30855));
#16163=CARTESIAN_POINT('Ctrl Pts',(0.233890236562906,0.154716040176168,
13.3244421875));
#16164=CARTESIAN_POINT('Ctrl Pts',(-0.00340698100913133,0.280410602722076,
13.340334375));
#16165=CARTESIAN_POINT('Ctrl Pts',(-0.237580284814888,0.148987628304026,
13.3562265625));
#16166=CARTESIAN_POINT('Ctrl Pts',(-0.253908499409691,-0.119046722735112,
13.37211875));
#16167=CARTESIAN_POINT('Ctrl Pts',(-0.0374201180154527,-0.277923634425439,
13.3880109375));
#16168=CARTESIAN_POINT('Ctrl Pts',(0.213380463928066,-0.18196281524805,
13.403903125));
#16169=CARTESIAN_POINT('Ctrl Pts',(0.268524639741408,0.0808441983795663,
13.4197953125));
#16170=CARTESIAN_POINT('Ctrl Pts',(0.077452087548127,0.269525343391667,
13.4356875));
#16171=CARTESIAN_POINT('Ctrl Pts',(-0.184643133777616,0.211064353693145,
13.4515796875));
#16172=CARTESIAN_POINT('Ctrl Pts',(-0.277424126375503,-0.0409164990464411,
13.467471875));
#16173=CARTESIAN_POINT('Ctrl Pts',(-0.115844693426342,-0.255404084499389,
13.4833640625));
#16174=CARTESIAN_POINT('Ctrl Pts',(0.151994963678255,-0.235653121630174,
13.49925625));
#16175=CARTESIAN_POINT('Ctrl Pts',(0.280386067331958,7.16919272130007E-5,
13.5151484375));
#16176=CARTESIAN_POINT('Ctrl Pts',(0.151848011613721,0.23594581398157,13.531040625));
#16177=CARTESIAN_POINT('Ctrl Pts',(-0.116259094268414,0.255025114686607,
13.5469328125));
#16178=CARTESIAN_POINT('Ctrl Pts',(-0.223221075339677,0.112500043789072,
13.5575276041667));
#16179=CARTESIAN_POINT('Ctrl Pts',(-0.234668236863856,0.0343918483395283,
13.562825));
#16180=CARTESIAN_POINT('',(0.137702479013109,-0.19310620885576,12.8));
#16181=CARTESIAN_POINT('Ctrl Pts',(0.137702479013109,-0.19310620885576,
12.8));
#16182=CARTESIAN_POINT('Ctrl Pts',(0.201976953076579,-0.147272600147639,
12.8052973958333));
#16183=CARTESIAN_POINT('Ctrl Pts',(0.279975622711063,0.012947463403363,
12.8158921875));
#16184=CARTESIAN_POINT('Ctrl Pts',(0.140636571093104,0.242795388419221,
12.831784375));
#16185=CARTESIAN_POINT('Ctrl Pts',(-0.127902988494662,0.249513882234533,
12.8476765625));
#16186=CARTESIAN_POINT('Ctrl Pts',(-0.233651108552229,0.0943166116198947,
12.8587954411032));
#16187=CARTESIAN_POINT('Ctrl Pts',(-0.237528617395594,0.0079260774111979,
12.864616923873));
#16188=CARTESIAN_POINT('Ctrl Pts',(-0.237475867347687,0.000143668378376506,
12.8651410108095));
#16189=CARTESIAN_POINT('Ctrl Pts',(0.129215683242003,0.264846751495042,
12.8));
#16190=CARTESIAN_POINT('Ctrl Pts',(0.135212459169762,0.261232067552344,
12.8));
#16191=CARTESIAN_POINT('Ctrl Pts',(0.141061626425574,0.257394031435174,
12.8));
#16192=CARTESIAN_POINT('Ctrl Pts',(0.146748920713232,0.253331893839978,
12.8));
#16193=CARTESIAN_POINT('Ctrl Pts',(0.15657328667399,0.246314861785777,12.8));
#16194=CARTESIAN_POINT('Ctrl Pts',(0.165915195693812,0.238629441830809,
12.8));
#16195=CARTESIAN_POINT('Ctrl Pts',(0.174740580578172,0.230346357604821,
12.8));
#16196=CARTESIAN_POINT('Ctrl Pts',(0.178901236248919,0.226441365153193,
12.8));
#16197=CARTESIAN_POINT('Ctrl Pts',(0.182946948479838,0.222403433701439,
12.8));
#16198=CARTESIAN_POINT('Ctrl Pts',(0.186873336456426,0.218239549379721,
12.8));
#16199=CARTESIAN_POINT('Ctrl Pts',(0.190449962393121,0.214446583235962,
12.8));
#16200=CARTESIAN_POINT('Ctrl Pts',(0.193924720399342,0.210551920535541,
12.8));
#16201=CARTESIAN_POINT('Ctrl Pts',(0.197289746551245,0.206567301120756,
12.8));
#16202=CARTESIAN_POINT('Ctrl Pts',(0.20843723213549,0.193367258838793,12.8));
#16203=CARTESIAN_POINT('Ctrl Pts',(0.218402335066749,0.179162279576202,
12.8));
#16204=CARTESIAN_POINT('Ctrl Pts',(0.227068433305708,0.164154641391987,
12.8));
#16205=CARTESIAN_POINT('Ctrl Pts',(0.230494359574639,0.158221745125157,
12.8));
#16206=CARTESIAN_POINT('Ctrl Pts',(0.233718830599218,0.152158127352311,
12.8));
#16207=CARTESIAN_POINT('Ctrl Pts',(0.236719485594126,0.146004799286039,
12.8));
#16208=CARTESIAN_POINT('Ctrl Pts',(0.244057081504557,0.130957872887894,
12.8));
#16209=CARTESIAN_POINT('Ctrl Pts',(0.250077313467251,0.115349535038238,
12.8));
#16210=CARTESIAN_POINT('Ctrl Pts',(0.254672578472357,0.0993652496009151,
12.8));
#16211=CARTESIAN_POINT('Ctrl Pts',(0.257632497295663,0.0890693934771714,
12.8));
#16212=CARTESIAN_POINT('Ctrl Pts',(0.260000238425513,0.0786172356827657,
12.8));
#16213=CARTESIAN_POINT('Ctrl Pts',(0.261735268122606,0.0680587419952843,
12.8));
#16214=CARTESIAN_POINT('Ctrl Pts',(0.26247802203292,0.0635387257174422,
12.8));
#16215=CARTESIAN_POINT('Ctrl Pts',(0.263104701090492,0.0589992464261977,
12.8));
#16216=CARTESIAN_POINT('Ctrl Pts',(0.263611560734367,0.0544443848764751,
12.8));
#16217=CARTESIAN_POINT('Ctrl Pts',(0.264100883204341,0.0500471200106794,
12.8));
#16218=CARTESIAN_POINT('Ctrl Pts',(0.264477472227069,0.0456446896458848,
12.8));
#16219=CARTESIAN_POINT('Ctrl Pts',(0.264739070133745,0.0412429691345073,
12.8));
#16220=CARTESIAN_POINT('Ctrl Pts',(0.265309177961261,0.0316501732671333,
12.8));
#16221=CARTESIAN_POINT('Ctrl Pts',(0.2653340197788,0.0220570104352547,12.8));
#16222=CARTESIAN_POINT('Ctrl Pts',(0.264787883227811,0.0125003360521388,
12.8));
#16223=CARTESIAN_POINT('Ctrl Pts',(0.263862534527666,-0.003692054298092,
12.8));
#16224=CARTESIAN_POINT('Ctrl Pts',(0.261300185398629,-0.019781536702279,
12.8));
#16225=CARTESIAN_POINT('Ctrl Pts',(0.257203559968843,-0.0355693262937758,
12.8));
#16226=CARTESIAN_POINT('Ctrl Pts',(0.256089106652214,-0.0398642648411328,
12.8));
#16227=CARTESIAN_POINT('Ctrl Pts',(0.254860056647025,-0.0441391928129072,
12.8));
#16228=CARTESIAN_POINT('Ctrl Pts',(0.253520584007838,-0.0483814917048708,
12.8));
#16229=CARTESIAN_POINT('Ctrl Pts',(0.248750211286509,-0.063489935369865,
12.8));
#16230=CARTESIAN_POINT('Ctrl Pts',(0.242605109706018,-0.0781226040481322,
12.8));
#16231=CARTESIAN_POINT('Ctrl Pts',(0.235197469927049,-0.0921011352816676,
12.8));
#16232=CARTESIAN_POINT('Ctrl Pts',(0.229495020889561,-0.10286189908183,
12.8));
#16233=CARTESIAN_POINT('Ctrl Pts',(0.223043166859496,-0.11323484442185,
12.8));
#16234=CARTESIAN_POINT('Ctrl Pts',(0.215878086649736,-0.123123415869591,
12.8));
#16235=CARTESIAN_POINT('Ctrl Pts',(0.213283707523951,-0.126703934523508,
12.8));
#16236=CARTESIAN_POINT('Ctrl Pts',(0.210594525319483,-0.130222266390069,
12.8));
#16237=CARTESIAN_POINT('Ctrl Pts',(0.207815760318832,-0.133668560993862,
12.8));
#16238=CARTESIAN_POINT('Ctrl Pts',(0.198088582382188,-0.145732452983772,
12.8));
#16239=CARTESIAN_POINT('Ctrl Pts',(0.187325168437807,-0.156846059287663,
12.8));
#16240=CARTESIAN_POINT('Ctrl Pts',(0.175614388817618,-0.166823177757923,
12.8));
#16241=CARTESIAN_POINT('Ctrl Pts',(0.16463984863336,-0.1761730495108,12.8));
#16242=CARTESIAN_POINT('Ctrl Pts',(0.152832183702603,-0.184525367271261,
12.8));
#16243=CARTESIAN_POINT('Ctrl Pts',(0.140246050763535,-0.191682120721285,
12.8));
#16244=CARTESIAN_POINT('Ctrl Pts',(0.139401695805602,-0.192162239617811,
12.8));
#16245=CARTESIAN_POINT('Ctrl Pts',(0.138553833519603,-0.1926369584628,12.8));
#16246=CARTESIAN_POINT('Ctrl Pts',(0.137702479013111,-0.193106208855758,
12.8));
#16247=CARTESIAN_POINT('Ctrl Pts',(0.0261206201035208,0.292499143797287,
13.5058));
#16248=CARTESIAN_POINT('Ctrl Pts',(0.0734750452512648,0.288342804146702,
13.5032390752998));
#16249=CARTESIAN_POINT('Ctrl Pts',(0.119860787283314,0.273336395466611,
13.5006781505996));
#16250=CARTESIAN_POINT('Ctrl Pts',(0.159503106385806,0.247855320894766,
13.4981172258995));
#16251=CARTESIAN_POINT('Ctrl Pts',(0.24150514885995,0.195146493393404,13.4928198300661));
#16252=CARTESIAN_POINT('Ctrl Pts',(0.294652818994247,0.0976177112587029,
13.4875224342328));
#16253=CARTESIAN_POINT('Ctrl Pts',(0.294683199723937,0.000119797020287853,
13.4822250383995));
#16254=CARTESIAN_POINT('Ctrl Pts',(0.294713580453626,-0.0973781172181258,
13.4769276425661));
#16255=CARTESIAN_POINT('Ctrl Pts',(0.241626671778709,-0.194845163560254,
13.4716302467328));
#16256=CARTESIAN_POINT('Ctrl Pts',(0.159710302139489,-0.247661981960665,
13.4663328508995));
#16257=CARTESIAN_POINT('Ctrl Pts',(0.0777939325002679,-0.300478800361077,
13.4610354550661));
#16258=CARTESIAN_POINT('Ctrl Pts',(-0.0329518981032568,-0.308645390819771,
13.4557380592328));
#16259=CARTESIAN_POINT('Ctrl Pts',(-0.121729591293106,-0.268385727164849,
13.4504406633995));
#16260=CARTESIAN_POINT('Ctrl Pts',(-0.210507284482955,-0.228126063509928,
13.4451432675661));
#16261=CARTESIAN_POINT('Ctrl Pts',(-0.277316840259129,-0.139440145741392,
13.4398458717328));
#16262=CARTESIAN_POINT('Ctrl Pts',(-0.291540164212148,-0.0430029056470576,
13.4345484758995));
#16263=CARTESIAN_POINT('Ctrl Pts',(-0.293626260696475,-0.0288587162730754,
13.4337715211693));
#16264=CARTESIAN_POINT('Ctrl Pts',(-0.29458115917577,-0.0145477859091552,
13.4329945664391));
#16265=CARTESIAN_POINT('Ctrl Pts',(-0.294460332090693,-0.000220795745557084,
13.432217611709));
#16266=CARTESIAN_POINT('Origin',(0.,0.,12.6151410108095));
#16267=CARTESIAN_POINT('',(-0.13770247901312,-0.193106208855752,12.8));
#16268=CARTESIAN_POINT('Ctrl Pts',(-0.138011838534631,-0.193375383177942,
12.8));
#16269=CARTESIAN_POINT('Ctrl Pts',(-0.0781015645619646,-0.235657681198368,
12.8049405016152));
#16270=CARTESIAN_POINT('Ctrl Pts',(0.0903526836839373,-0.26250844141701,
12.8151859925577));
#16271=CARTESIAN_POINT('Ctrl Pts',(0.271186343139681,-0.0718941087923526,
12.8307364728275));
#16272=CARTESIAN_POINT('Ctrl Pts',(0.207021633736509,0.189392429248662,
12.8466514408095));
#16273=CARTESIAN_POINT('Ctrl Pts',(-0.0475028660546131,0.276509970564655,
12.8625664087915));
#16274=CARTESIAN_POINT('Ctrl Pts',(-0.216222593118796,0.142818607294397,
12.8753022582519));
#16275=CARTESIAN_POINT('Ctrl Pts',(-0.237002089177395,0.0319078962725245,
12.8827331183849));
#16276=CARTESIAN_POINT('Ctrl Pts',(-0.23685325391662,0.000124198907147644,
12.8848589891905));
#16277=CARTESIAN_POINT('Origin',(0.,0.,12.8));
#16278=CARTESIAN_POINT('Ctrl Pts',(-0.103908919352494,0.213201587949051,
12.7670766008995));
#16279=CARTESIAN_POINT('Ctrl Pts',(-0.174973765135383,0.178566426924752,
12.7723815902268));
#16280=CARTESIAN_POINT('Ctrl Pts',(-0.278449645037139,0.0331055665616523,
12.7829915688815));
#16281=CARTESIAN_POINT('Ctrl Pts',(-0.178281517311376,-0.216843324364553,
12.7989065368635));
#16282=CARTESIAN_POINT('Ctrl Pts',(0.086114123480329,-0.26697625082225,
12.8148215048455));
#16283=CARTESIAN_POINT('Ctrl Pts',(0.271186343139681,-0.0718941087923526,
12.8307364728275));
#16284=CARTESIAN_POINT('Ctrl Pts',(0.207021633736509,0.189392429248662,
12.8466514408095));
#16285=CARTESIAN_POINT('Ctrl Pts',(-0.0475028660546131,0.276509970564655,
12.8625664087915));
#16286=CARTESIAN_POINT('Ctrl Pts',(-0.258338355475561,0.109446613499621,
12.8784813767735));
#16287=CARTESIAN_POINT('Ctrl Pts',(-0.231681731794662,-0.158247829181543,
12.8943963447556));
#16288=CARTESIAN_POINT('Ctrl Pts',(0.00797328488061451,-0.280452709922419,
12.9103113127376));
#16289=CARTESIAN_POINT('Ctrl Pts',(0.240296121102423,-0.14482920233622,
12.9262262807196));
#16290=CARTESIAN_POINT('Ctrl Pts',(0.251706166281744,0.123942967091746,
12.9421412487016));
#16291=CARTESIAN_POINT('Ctrl Pts',(0.0317122558575804,0.278768752799521,
12.9580562166836));
#16292=CARTESIAN_POINT('Ctrl Pts',(-0.21743576073689,0.177311681816183,
12.9739711846656));
#16293=CARTESIAN_POINT('Ctrl Pts',(-0.266686554811307,-0.0871552256344479,
12.9898861526476));
#16294=CARTESIAN_POINT('Ctrl Pts',(-0.0707617483345123,-0.271496792539298,
13.0058011206296));
#16295=CARTESIAN_POINT('Ctrl Pts',(0.19021711870995,-0.20624060859311,13.0217160886116));
#16296=CARTESIAN_POINT('Ctrl Pts',(0.276321843237659,0.0486207800379639,
13.0376310565936));
#16297=CARTESIAN_POINT('Ctrl Pts',(0.108392911780422,0.258783144727794,
13.0535460245757));
#16298=CARTESIAN_POINT('Ctrl Pts',(-0.159185927336213,0.231035886385667,
13.0694609925577));
#16299=CARTESIAN_POINT('Ctrl Pts',(-0.280418819849278,-0.0091118443472218,
13.0853759605397));
#16300=CARTESIAN_POINT('Ctrl Pts',(-0.143851548471854,-0.240882693501056,
13.1012909285217));
#16301=CARTESIAN_POINT('Ctrl Pts',(0.124964166840451,-0.25120051183695,
13.1172058965037));
#16302=CARTESIAN_POINT('Ctrl Pts',(0.278895358440525,-0.030579718254803,
13.1331208644857));
#16303=CARTESIAN_POINT('Ctrl Pts',(0.176426965387693,0.218154225247527,
13.1490358324677));
#16304=CARTESIAN_POINT('Ctrl Pts',(-0.0882377470317194,0.266330321450576,
13.1649508004497));
#16305=CARTESIAN_POINT('Ctrl Pts',(-0.271781992573435,0.0696583707968577,
13.1808657684317));
#16306=CARTESIAN_POINT('Ctrl Pts',(-0.205466253473662,-0.191053287885107,
13.1967807364137));
#16307=CARTESIAN_POINT('Ctrl Pts',(0.0497427765240963,-0.276122067797826,
13.2126957043958));
#16308=CARTESIAN_POINT('Ctrl Pts',(0.259221295320457,-0.107340859314887,
13.2286106723778));
#16309=CARTESIAN_POINT('Ctrl Pts',(0.23038737805747,0.160123065998856,13.2445256403598));
#16310=CARTESIAN_POINT('Ctrl Pts',(-0.0102508111899536,0.280379494845555,
13.2604406083418));
#16311=CARTESIAN_POINT('Ctrl Pts',(-0.241465019981373,0.14287191272199,
13.2763555763238));
#16312=CARTESIAN_POINT('Ctrl Pts',(-0.250690846589451,-0.125983493910996,
13.2922705443058));
#16313=CARTESIAN_POINT('Ctrl Pts',(-0.0294466067184147,-0.279017272289624,
13.3081855122878));
#16314=CARTESIAN_POINT('Ctrl Pts',(0.218869047461476,-0.175539378629952,
13.3241004802698));
#16315=CARTESIAN_POINT('Ctrl Pts',(0.265969733682413,0.0893188257727471,
13.3400154482518));
#16316=CARTESIAN_POINT('Ctrl Pts',(0.0685537852907199,0.272062715339731,
13.3559304162339));
#16317=CARTESIAN_POINT('Ctrl Pts',(-0.191886195286831,0.204688477368222,
13.3718453842159));
#16318=CARTESIAN_POINT('Ctrl Pts',(-0.275917956826614,-0.0508638804691982,
13.3877603521979));
#16319=CARTESIAN_POINT('Ctrl Pts',(-0.106286584194727,-0.259655320928406,
13.4036753201799));
#16320=CARTESIAN_POINT('Ctrl Pts',(0.161056632784338,-0.229734753162831,
13.4195902881619));
#16321=CARTESIAN_POINT('Ctrl Pts',(0.280337460803119,0.0113889577443968,
13.4355052561439));
#16322=CARTESIAN_POINT('Ctrl Pts',(0.141885966824002,0.242044705653255,
13.4514202241259));
#16323=CARTESIAN_POINT('Ctrl Pts',(-0.126992591218768,0.250174275017661,
13.4673351921079));
#16324=CARTESIAN_POINT('Ctrl Pts',(-0.279151391016313,0.0283187214630216,
13.4832501600899));
#16325=CARTESIAN_POINT('Ctrl Pts',(-0.17461423217311,-0.219592043360215,
13.499165128072));
#16326=CARTESIAN_POINT('Ctrl Pts',(0.0903269506402298,-0.265580501456578,
13.515080096054));
#16327=CARTESIAN_POINT('Ctrl Pts',(0.272486967933624,-0.0674994743880085,
13.530995064036));
#16328=CARTESIAN_POINT('Ctrl Pts',(0.203600577200948,0.19281335099551,13.546910032018));
#16329=CARTESIAN_POINT('Ctrl Pts',(0.0337423613347716,0.2477160478489,13.5575200106727));
#16330=CARTESIAN_POINT('Ctrl Pts',(-0.043944522199392,0.233068358199193,
13.562825));
#16331=CARTESIAN_POINT('Ctrl Pts',(-0.112236674703431,0.230288577939276,
12.7780510672663));
#16332=CARTESIAN_POINT('Ctrl Pts',(-0.18899699546017,0.192877590264599,
12.7833560565936));
#16333=CARTESIAN_POINT('Ctrl Pts',(-0.300765924870234,0.0357588042316975,
12.7939660352483));
#16334=CARTESIAN_POINT('Ctrl Pts',(-0.19256984663878,-0.234222180443943,
12.8098810032303));
#16335=CARTESIAN_POINT('Ctrl Pts',(0.0930157191958205,-0.288372998235396,
12.8257959712123));
#16336=CARTESIAN_POINT('Ctrl Pts',(0.292920507389061,-0.0776560448506564,
12.8417109391944));
#16337=CARTESIAN_POINT('Ctrl Pts',(0.223613332782678,0.204571239941054,
12.8576259071764));
#16338=CARTESIAN_POINT('Ctrl Pts',(-0.0513099718299037,0.298670795653654,
12.8735408751584));
#16339=CARTESIAN_POINT('Ctrl Pts',(-0.279042820843599,0.118218186016141,
12.8894558431404));
#16340=CARTESIAN_POINT('Ctrl Pts',(-0.250249808468835,-0.170930563391974,
12.9053708111224));
#16341=CARTESIAN_POINT('Ctrl Pts',(0.00861230187975927,-0.302929524908998,
12.9212857791044));
#16342=CARTESIAN_POINT('Ctrl Pts',(0.259554595935866,-0.156436503925375,
12.9372007470864));
#16343=CARTESIAN_POINT('Ctrl Pts',(0.271879096441916,0.133876346380466,
12.9531157150684));
#16344=CARTESIAN_POINT('Ctrl Pts',(0.0342538269763452,0.301110607447485,
12.9690306830504));
#16345=CARTESIAN_POINT('Ctrl Pts',(-0.234862097486857,0.191522283911076,
12.9849456510324));
#16346=CARTESIAN_POINT('Ctrl Pts',(-0.28806008460733,-0.0941402602316915,
13.0008606190145));
#16347=CARTESIAN_POINT('Ctrl Pts',(-0.0764329316362602,-0.293255837681146,
13.0167755869965));
#16348=CARTESIAN_POINT('Ctrl Pts',(0.205462023940876,-0.222769712567,13.0326905549785));
#16349=CARTESIAN_POINT('Ctrl Pts',(0.298467590907281,0.0525174807605868,
13.0486055229605));
#16350=CARTESIAN_POINT('Ctrl Pts',(0.117080035626076,0.279523257623478,
13.0645204909425));
#16351=CARTESIAN_POINT('Ctrl Pts',(-0.171943845197633,0.249552201934865,
13.0804354589245));
#16352=CARTESIAN_POINT('Ctrl Pts',(-0.302892918724096,-0.00984211092098895,
13.0963504269065));
#16353=CARTESIAN_POINT('Ctrl Pts',(-0.155380496227179,-0.260188179038313,
13.1122653948885));
#16354=CARTESIAN_POINT('Ctrl Pts',(0.134979389937427,-0.271332916443256,
13.1281803628705));
#16355=CARTESIAN_POINT('Ctrl Pts',(0.301247359867139,-0.0330305224197738,
13.1440953308526));
#16356=CARTESIAN_POINT('Ctrl Pts',(0.190566662097203,0.235638143162905,
13.1600102988346));
#16357=CARTESIAN_POINT('Ctrl Pts',(-0.095309540045996,0.287675301009579,
13.1759252668166));
#16358=CARTESIAN_POINT('Ctrl Pts',(-0.293563895003427,0.0752411241712175,
13.1918402347986));
#16359=CARTESIAN_POINT('Ctrl Pts',(-0.22193329694274,-0.206365207693472,
13.2077552027806));
#16360=CARTESIAN_POINT('Ctrl Pts',(0.0537293993852549,-0.298251804512869,
13.2236701707626));
#16361=CARTESIAN_POINT('Ctrl Pts',(0.279996523690013,-0.115943666668714,
13.2395851387446));
#16362=CARTESIAN_POINT('Ctrl Pts',(0.248851719062674,0.172956090613008,
13.2555001067266));
#16363=CARTESIAN_POINT('Ctrl Pts',(-0.0110723599874049,0.302850442027407,
13.2714150747086));
#16364=CARTESIAN_POINT('Ctrl Pts',(-0.260817175934343,0.15432234780575,
13.2873300426906));
#16365=CARTESIAN_POINT('Ctrl Pts',(-0.270782404197074,-0.136080410730889,
13.3032450106727));
#16366=CARTESIAN_POINT('Ctrl Pts',(-0.0318065979318202,-0.301379044472352,
13.3191599786547));
#16367=CARTESIAN_POINT('Ctrl Pts',(0.236410254631274,-0.189607939912231,
13.3350749466367));
#16368=CARTESIAN_POINT('Ctrl Pts',(0.287285814021459,0.096477261582719,
13.3509899146187));
#16369=CARTESIAN_POINT('Ctrl Pts',(0.0740480119253485,0.293867116228312,
13.3669048826007));
#16370=CARTESIAN_POINT('Ctrl Pts',(-0.20726486825859,0.221093186158389,
13.3828198505827));
#16371=CARTESIAN_POINT('Ctrl Pts',(-0.298031335116959,-0.0549403539364065,
13.3987348185647));
#16372=CARTESIAN_POINT('Ctrl Pts',(-0.114804896922607,-0.280465334175926,
13.4146497865467));
#16373=CARTESIAN_POINT('Ctrl Pts',(0.173964477883985,-0.248146789702814,
13.4305647545288));
#16374=CARTESIAN_POINT('Ctrl Pts',(0.302805039176751,0.0123017230237244,
13.4464797225107));
#16375=CARTESIAN_POINT('Ctrl Pts',(0.153257383510892,0.261443320374982,
13.4623946904928));
#16376=CARTESIAN_POINT('Ctrl Pts',(-0.137170381899699,0.2702244321209,13.4783096584748));
#16377=CARTESIAN_POINT('Ctrl Pts',(-0.301523912112135,0.030588318583895,
13.4942246264568));
#16378=CARTESIAN_POINT('Ctrl Pts',(-0.188608647815107,-0.237191194862433,
13.5101395944388));
#16379=CARTESIAN_POINT('Ctrl Pts',(0.0975661823752476,-0.286865386872497,
13.5260545624208));
#16380=CARTESIAN_POINT('Ctrl Pts',(0.294325370444308,-0.0729092035289056,
13.5419695304028));
#16381=CARTESIAN_POINT('Ctrl Pts',(0.219918096493853,0.208266330638556,
13.5578844983848));
#16382=CARTESIAN_POINT('Ctrl Pts',(0.0364466347687562,0.267569190926913,
13.5684944770395));
#16383=CARTESIAN_POINT('Ctrl Pts',(-0.0474664453622039,0.251747565713066,
13.5737994663668));
#16384=CARTESIAN_POINT('Ctrl Pts',(-0.120564430054368,0.247375567929501,
12.7890255336332));
#16385=CARTESIAN_POINT('Ctrl Pts',(-0.203020225784959,0.207188753604445,
12.7943305229605));
#16386=CARTESIAN_POINT('Ctrl Pts',(-0.323082204703329,0.0384120419017428,
12.8049405016152));
#16387=CARTESIAN_POINT('Ctrl Pts',(-0.206858175966185,-0.251601036523333,
12.8208554695972));
#16388=CARTESIAN_POINT('Ctrl Pts',(0.0999173149113121,-0.309769745648542,
12.8367704375792));
#16389=CARTESIAN_POINT('Ctrl Pts',(0.314654671638441,-0.0834179809089602,
12.8526854055612));
#16390=CARTESIAN_POINT('Ctrl Pts',(0.240205031828846,0.219750050633447,
12.8686003735432));
#16391=CARTESIAN_POINT('Ctrl Pts',(-0.0551170776051942,0.320831620742652,
12.8845153415252));
#16392=CARTESIAN_POINT('Ctrl Pts',(-0.299747286211637,0.12698975853266,
12.9004303095072));
#16393=CARTESIAN_POINT('Ctrl Pts',(-0.268817885143008,-0.183613297602405,
12.9163452774892));
#16394=CARTESIAN_POINT('Ctrl Pts',(0.00925131887890369,-0.325406339895578,
12.9322602454712));
#16395=CARTESIAN_POINT('Ctrl Pts',(0.278813070769308,-0.16804380551453,
12.9481752134533));
#16396=CARTESIAN_POINT('Ctrl Pts',(0.292052026602089,0.143809725669185,
12.9640901814353));
#16397=CARTESIAN_POINT('Ctrl Pts',(0.0367953980951103,0.323452462095449,
12.9800051494173));
#16398=CARTESIAN_POINT('Ctrl Pts',(-0.252288434236825,0.205732886005968,
12.9959201173993));
#16399=CARTESIAN_POINT('Ctrl Pts',(-0.309433614403352,-0.101125294828935,
13.0118350853813));
#16400=CARTESIAN_POINT('Ctrl Pts',(-0.0821041149380083,-0.315014882822994,
13.0277500533633));
#16401=CARTESIAN_POINT('Ctrl Pts',(0.220706929171802,-0.239298816540891,
13.0436650213453));
#16402=CARTESIAN_POINT('Ctrl Pts',(0.320613338576903,0.0564141814832096,
13.0595799893273));
#16403=CARTESIAN_POINT('Ctrl Pts',(0.125767159471731,0.300263370519163,
13.0754949573094));
#16404=CARTESIAN_POINT('Ctrl Pts',(-0.184701763059053,0.268068517484062,
13.0914099252914));
#16405=CARTESIAN_POINT('Ctrl Pts',(-0.325367017598915,-0.010572377494756,
13.1073248932734));
#16406=CARTESIAN_POINT('Ctrl Pts',(-0.166909443982505,-0.279493664575571,
13.1232398612554));
#16407=CARTESIAN_POINT('Ctrl Pts',(0.144994613034403,-0.291465321049563,
13.1391548292374));
#16408=CARTESIAN_POINT('Ctrl Pts',(0.323599361293752,-0.0354813265847442,
13.1550697972194));
#16409=CARTESIAN_POINT('Ctrl Pts',(0.204706358806712,0.253122061078283,
13.1709847652014));
#16410=CARTESIAN_POINT('Ctrl Pts',(-0.102381333060272,0.309020280568582,
13.1868997331834));
#16411=CARTESIAN_POINT('Ctrl Pts',(-0.315345797433419,0.0808238775455775,
13.2028147011654));
#16412=CARTESIAN_POINT('Ctrl Pts',(-0.238400340411818,-0.221677127501839,
13.2187296691474));
#16413=CARTESIAN_POINT('Ctrl Pts',(0.0577160222464135,-0.320381541227913,
13.2346446371294));
#16414=CARTESIAN_POINT('Ctrl Pts',(0.30077175205957,-0.124546474022541,
13.2505596051115));
#16415=CARTESIAN_POINT('Ctrl Pts',(0.267316060067878,0.185789115227159,
13.2664745730935));
#16416=CARTESIAN_POINT('Ctrl Pts',(-0.0118939087848559,0.32532138920926,
13.2823895410755));
#16417=CARTESIAN_POINT('Ctrl Pts',(-0.280169331887314,0.16577278288951,
13.2983045090575));
#16418=CARTESIAN_POINT('Ctrl Pts',(-0.290873961804697,-0.146177327550781,
13.3142194770395));
#16419=CARTESIAN_POINT('Ctrl Pts',(-0.0341665891452253,-0.323740816655081,
13.3301344450215));
#16420=CARTESIAN_POINT('Ctrl Pts',(0.253951461801071,-0.20367650119451,
13.3460494130035));
#16421=CARTESIAN_POINT('Ctrl Pts',(0.308601894360506,0.103635697392691,
13.3619643809855));
#16422=CARTESIAN_POINT('Ctrl Pts',(0.0795422385599767,0.315671517116894,
13.3778793489676));
#16423=CARTESIAN_POINT('Ctrl Pts',(-0.22264354123035,0.237497894948556,
13.3937943169495));
#16424=CARTESIAN_POINT('Ctrl Pts',(-0.320144713407304,-0.0590168274036149,
13.4097092849316));
#16425=CARTESIAN_POINT('Ctrl Pts',(-0.123323209650487,-0.301275347423447,
13.4256242529136));
#16426=CARTESIAN_POINT('Ctrl Pts',(0.186872322983632,-0.266558826242796,
13.4415392208956));
#16427=CARTESIAN_POINT('Ctrl Pts',(0.325272617550382,0.013214488303052,
13.4574541888776));
#16428=CARTESIAN_POINT('Ctrl Pts',(0.164628800197782,0.280841935096709,
13.4733691568596));
#16429=CARTESIAN_POINT('Ctrl Pts',(-0.14734817258063,0.290274589224139,
13.4892841248416));
#16430=CARTESIAN_POINT('Ctrl Pts',(-0.323896433207958,0.0328579157047686,
13.5051990928236));
#16431=CARTESIAN_POINT('Ctrl Pts',(-0.202603063457104,-0.254790346364651,
13.5211140608057));
#16432=CARTESIAN_POINT('Ctrl Pts',(0.104805414110265,-0.308150272288416,
13.5370290287877));
#16433=CARTESIAN_POINT('Ctrl Pts',(0.316163772954992,-0.0783189326698027,
13.5529439967697));
#16434=CARTESIAN_POINT('Ctrl Pts',(0.236235615786759,0.223719310281602,
13.5688589647517));
#16435=CARTESIAN_POINT('Ctrl Pts',(0.0391509082027412,0.287422334004927,
13.5794689434064));
#16436=CARTESIAN_POINT('Ctrl Pts',(-0.0509883685250158,0.27042677322694,
13.5847739327337));
#16437=CARTESIAN_POINT('Ctrl Pts',(-0.128892185405305,0.264462557919726,
12.8));
#16438=CARTESIAN_POINT('Ctrl Pts',(-0.217043456109746,0.221499916944292,
12.8053049893273));
#16439=CARTESIAN_POINT('Ctrl Pts',(-0.345398484536424,0.0410652795717879,
12.815914967982));
#16440=CARTESIAN_POINT('Ctrl Pts',(-0.22114650529359,-0.268979892602724,
12.831829935964));
#16441=CARTESIAN_POINT('Ctrl Pts',(0.106818910626803,-0.331166493061688,
12.847744903946));
#16442=CARTESIAN_POINT('Ctrl Pts',(0.336388835887821,-0.0891799169672639,
12.863659871928));
#16443=CARTESIAN_POINT('Ctrl Pts',(0.256796730875014,0.234928861325839,
12.8795748399101));
#16444=CARTESIAN_POINT('Ctrl Pts',(-0.0589241833804849,0.34299244583165,
12.8954898078921));
#16445=CARTESIAN_POINT('Ctrl Pts',(-0.320451751579676,0.13576133104918,
12.9114047758741));
#16446=CARTESIAN_POINT('Ctrl Pts',(-0.287385961817181,-0.196296031812836,
12.9273197438561));
#16447=CARTESIAN_POINT('Ctrl Pts',(0.00989033587804837,-0.347883154882157,
12.9432347118381));
#16448=CARTESIAN_POINT('Ctrl Pts',(0.298071545602751,-0.179651107103685,
12.9591496798201));
#16449=CARTESIAN_POINT('Ctrl Pts',(0.312224956762261,0.153743104957905,
12.9750646478021));
#16450=CARTESIAN_POINT('Ctrl Pts',(0.0393369692138751,0.345794316743414,
12.9909796157841));
#16451=CARTESIAN_POINT('Ctrl Pts',(-0.269714770986793,0.219943488100861,
13.0068945837661));
#16452=CARTESIAN_POINT('Ctrl Pts',(-0.330807144199375,-0.108110329426179,
13.0228095517481));
#16453=CARTESIAN_POINT('Ctrl Pts',(-0.0877752982397562,-0.336773927964842,
13.0387245197302));
#16454=CARTESIAN_POINT('Ctrl Pts',(0.235951834402727,-0.255827920514781,
13.0546394877122));
#16455=CARTESIAN_POINT('Ctrl Pts',(0.342759086246525,0.0603108822058324,
13.0705544556942));
#16456=CARTESIAN_POINT('Ctrl Pts',(0.134454283317385,0.321003483414848,
13.0864694236762));
#16457=CARTESIAN_POINT('Ctrl Pts',(-0.197459680920473,0.28658483303326,
13.1023843916582));
#16458=CARTESIAN_POINT('Ctrl Pts',(-0.347841116473733,-0.0113026440685232,
13.1182993596402));
#16459=CARTESIAN_POINT('Ctrl Pts',(-0.178438391737831,-0.298799150112829,
13.1342143276222));
#16460=CARTESIAN_POINT('Ctrl Pts',(0.15500983613138,-0.311597725655869,
13.1501292956042));
#16461=CARTESIAN_POINT('Ctrl Pts',(0.345951362720365,-0.0379321307497152,
13.1660442635862));
#16462=CARTESIAN_POINT('Ctrl Pts',(0.218846055516222,0.270605978993662,
13.1819592315683));
#16463=CARTESIAN_POINT('Ctrl Pts',(-0.109453126074549,0.330365260127584,
13.1978741995503));
#16464=CARTESIAN_POINT('Ctrl Pts',(-0.33712769986341,0.0864066309199375,
13.2137891675323));
#16465=CARTESIAN_POINT('Ctrl Pts',(-0.254867383880897,-0.236989047310205,
13.2297041355143));
#16466=CARTESIAN_POINT('Ctrl Pts',(0.0617026451075722,-0.342511277942956,
13.2456191034963));
#16467=CARTESIAN_POINT('Ctrl Pts',(0.321546980429126,-0.133149281376369,
13.2615340714783));
#16468=CARTESIAN_POINT('Ctrl Pts',(0.285780401073082,0.198622139841311,
13.2774490394603));
#16469=CARTESIAN_POINT('Ctrl Pts',(-0.0127154575823072,0.347792336391113,
13.2933640074423));
#16470=CARTESIAN_POINT('Ctrl Pts',(-0.299521487840284,0.177223217973269,
13.3092789754243));
#16471=CARTESIAN_POINT('Ctrl Pts',(-0.31096551941232,-0.156274244370674,
13.3251939434064));
#16472=CARTESIAN_POINT('Ctrl Pts',(-0.0365265803586308,-0.346102588837809,
13.3411089113884));
#16473=CARTESIAN_POINT('Ctrl Pts',(0.271492668970869,-0.217745062476789,
13.3570238793704));
#16474=CARTESIAN_POINT('Ctrl Pts',(0.329917974699552,0.110794133202663,
13.3729388473524));
#16475=CARTESIAN_POINT('Ctrl Pts',(0.0850364651946051,0.337475918005475,
13.3888538153344));
#16476=CARTESIAN_POINT('Ctrl Pts',(-0.238022214202109,0.253902603738722,
13.4047687833164));
#16477=CARTESIAN_POINT('Ctrl Pts',(-0.34225809169765,-0.0630933008708229,
13.4206837512984));
#16478=CARTESIAN_POINT('Ctrl Pts',(-0.131841522378367,-0.322085360670968,
13.4365987192804));
#16479=CARTESIAN_POINT('Ctrl Pts',(0.199780168083279,-0.284970862782778,
13.4525136872625));
#16480=CARTESIAN_POINT('Ctrl Pts',(0.347740195924013,0.0141272535823796,
13.4684286552444));
#16481=CARTESIAN_POINT('Ctrl Pts',(0.176000216884672,0.300240549818435,
13.4843436232265));
#16482=CARTESIAN_POINT('Ctrl Pts',(-0.157525963261562,0.310324746327379,
13.5002585912085));
#16483=CARTESIAN_POINT('Ctrl Pts',(-0.34626895430378,0.035127512825642,
13.5161735591905));
#16484=CARTESIAN_POINT('Ctrl Pts',(-0.216597479099101,-0.27238949786687,
13.5320885271725));
#16485=CARTESIAN_POINT('Ctrl Pts',(0.112044645845283,-0.329435157704335,
13.5480034951545));
#16486=CARTESIAN_POINT('Ctrl Pts',(0.338002175465677,-0.0837286618106999,
13.5639184631365));
#16487=CARTESIAN_POINT('Ctrl Pts',(0.252553135079664,0.239172289924649,
13.5798334311185));
#16488=CARTESIAN_POINT('Ctrl Pts',(0.0418551816367257,0.30727547708294,
13.5904434097732));
#16489=CARTESIAN_POINT('Ctrl Pts',(-0.0545102916878278,0.289105980740814,
13.5957483991005));
#16490=CARTESIAN_POINT('Ctrl Pts',(-0.294362671296069,-0.000253937998619662,
13.417782388291));
#16491=CARTESIAN_POINT('Ctrl Pts',(-0.294525507057634,-0.0181030578418672,
13.4187495092935));
#16492=CARTESIAN_POINT('Ctrl Pts',(-0.293042212129893,-0.035925170963799,
13.419716630296));
#16493=CARTESIAN_POINT('Ctrl Pts',(-0.289816017228513,-0.0534259934025893,
13.4206837512984));
#16494=CARTESIAN_POINT('Ctrl Pts',(-0.272119235257889,-0.149423987470871,
13.4259887406258));
#16495=CARTESIAN_POINT('Ctrl Pts',(-0.201980378818128,-0.235754674070919,
13.4312937299531));
#16496=CARTESIAN_POINT('Ctrl Pts',(-0.111640668854641,-0.272734267722911,
13.4365987192804));
#16497=CARTESIAN_POINT('Ctrl Pts',(-0.0213009588911521,-0.309713861374905,
13.4419037086078));
#16498=CARTESIAN_POINT('Ctrl Pts',(0.089239604596064,-0.297342362078841,
13.4472086979351));
#16499=CARTESIAN_POINT('Ctrl Pts',(0.169169890979795,-0.241306926369949,
13.4525136872624));
#16500=CARTESIAN_POINT('Ctrl Pts',(0.249100177363524,-0.185271490661058,
13.4578186765898));
#16501=CARTESIAN_POINT('Ctrl Pts',(0.298420186643769,-0.0855721185393391,
13.4631236659171));
#16502=CARTESIAN_POINT('Ctrl Pts',(0.294456861444001,0.011963116894196,
13.4684286552444));
#16503=CARTESIAN_POINT('Ctrl Pts',(0.290493536244233,0.109498352327731,
13.4737336445718));
#16504=CARTESIAN_POINT('Ctrl Pts',(0.233246876564453,0.204869451073082,
13.4790386338991));
#16505=CARTESIAN_POINT('Ctrl Pts',(0.149035850033524,0.254235699863916,
13.4843436232265));
#16506=CARTESIAN_POINT('Ctrl Pts',(0.0648248235025946,0.30360194865475,
13.4896486125538));
#16507=CARTESIAN_POINT('Ctrl Pts',(-0.0463505698794843,0.306963347491064,
13.4949536018811));
#16508=CARTESIAN_POINT('Ctrl Pts',(-0.133395431744227,0.262777841325598,
13.5002585912085));
#16509=CARTESIAN_POINT('Ctrl Pts',(-0.163703451423551,0.247392956316707,
13.5021057274723));
#16510=CARTESIAN_POINT('Ctrl Pts',(-0.191086000567156,0.226243711349668,
13.5039528637362));
#16511=CARTESIAN_POINT('Ctrl Pts',(-0.214321504642992,0.201109806014066,
13.5058));
#16512=CARTESIAN_POINT('Ctrl Pts',(-0.138011838534635,-0.19337538317794,
12.8));
#16513=CARTESIAN_POINT('Ctrl Pts',(-0.142822234716732,-0.190758128899072,
12.8));
#16514=CARTESIAN_POINT('Ctrl Pts',(-0.147526903047439,-0.187967753105685,
12.8));
#16515=CARTESIAN_POINT('Ctrl Pts',(-0.1521153417148,-0.185006306498425,
12.8));
#16516=CARTESIAN_POINT('Ctrl Pts',(-0.162156783890052,-0.178525410268204,
12.8));
#16517=CARTESIAN_POINT('Ctrl Pts',(-0.171642243951589,-0.17122677990977,
12.8));
#16518=CARTESIAN_POINT('Ctrl Pts',(-0.18054346266442,-0.163220362486912,
12.8));
#16519=CARTESIAN_POINT('Ctrl Pts',(-0.185992032158252,-0.158319514284835,
12.8));
#16520=CARTESIAN_POINT('Ctrl Pts',(-0.191225243452385,-0.153148297109027,
12.8));
#16521=CARTESIAN_POINT('Ctrl Pts',(-0.196212723907213,-0.147754132341615,
12.8));
#16522=CARTESIAN_POINT('Ctrl Pts',(-0.202978562151886,-0.140436600651622,
12.8));
#16523=CARTESIAN_POINT('Ctrl Pts',(-0.209300021277213,-0.132703531992446,
12.8));
#16524=CARTESIAN_POINT('Ctrl Pts',(-0.215160567422495,-0.124614033470671,
12.8));
#16525=CARTESIAN_POINT('Ctrl Pts',(-0.218668715917161,-0.119771624357552,
12.8));
#16526=CARTESIAN_POINT('Ctrl Pts',(-0.222011627016975,-0.114801320422425,
12.8));
#16527=CARTESIAN_POINT('Ctrl Pts',(-0.225184859023271,-0.109714472354803,
12.8));
#16528=CARTESIAN_POINT('Ctrl Pts',(-0.228211935744122,-0.104861918448424,
12.8));
#16529=CARTESIAN_POINT('Ctrl Pts',(-0.231085348796075,-0.0999011605270764,
12.8));
#16530=CARTESIAN_POINT('Ctrl Pts',(-0.233790550755382,-0.09486224802396,
12.8));
#16531=CARTESIAN_POINT('Ctrl Pts',(-0.241364933609335,-0.0807536331995264,
12.8));
#16532=CARTESIAN_POINT('Ctrl Pts',(-0.247644353527102,-0.0660037746918586,
12.8));
#16533=CARTESIAN_POINT('Ctrl Pts',(-0.252557798454291,-0.0508304825079511,
12.8));
#16534=CARTESIAN_POINT('Ctrl Pts',(-0.255926241889587,-0.0404283354998718,
12.8));
#16535=CARTESIAN_POINT('Ctrl Pts',(-0.258652125794692,-0.0298261112740156,
12.8));
#16536=CARTESIAN_POINT('Ctrl Pts',(-0.260701325119157,-0.0190856734862765,
12.8));
#16537=CARTESIAN_POINT('Ctrl Pts',(-0.26182904176174,-0.0131749891046926,
12.8));
#16538=CARTESIAN_POINT('Ctrl Pts',(-0.262751878512061,-0.00721720616864429,
12.8));
#16539=CARTESIAN_POINT('Ctrl Pts',(-0.26346009243944,-0.00125328645715371,
12.8));
#16540=CARTESIAN_POINT('Ctrl Pts',(-0.264745555031066,0.00957168519646787,
12.8));
#16541=CARTESIAN_POINT('Ctrl Pts',(-0.265328748128811,0.0204329089429716,
12.8));
#16542=CARTESIAN_POINT('Ctrl Pts',(-0.265185345887169,0.0312672356517,12.8));
#16543=CARTESIAN_POINT('Ctrl Pts',(-0.265031299079076,0.042905780685675,
12.8));
#16544=CARTESIAN_POINT('Ctrl Pts',(-0.264039219970955,0.0545135318648275,
12.8));
#16545=CARTESIAN_POINT('Ctrl Pts',(-0.262262766017228,0.066031106495167,
12.8));
#16546=CARTESIAN_POINT('Ctrl Pts',(-0.261137536932211,0.0733264883629122,
12.8));
#16547=CARTESIAN_POINT('Ctrl Pts',(-0.25969728945567,0.0805857612874066,
12.8));
#16548=CARTESIAN_POINT('Ctrl Pts',(-0.257952591865992,0.0877939534757336,
12.8));
#16549=CARTESIAN_POINT('Ctrl Pts',(-0.256901952665834,0.0921346537324037,
12.8));
#16550=CARTESIAN_POINT('Ctrl Pts',(-0.255740653864154,0.0964566832907016,
12.8));
#16551=CARTESIAN_POINT('Ctrl Pts',(-0.254475469588544,0.100742853504323,
12.8));
#16552=CARTESIAN_POINT('Ctrl Pts',(-0.249793608361451,0.116603984979587,
12.8));
#16553=CARTESIAN_POINT('Ctrl Pts',(-0.243682406310052,0.132021898855319,
12.8));
#16554=CARTESIAN_POINT('Ctrl Pts',(-0.23628872388492,0.146835744613901,
12.8));
#16555=CARTESIAN_POINT('Ctrl Pts',(-0.229571591801449,0.160294066584336,
12.8));
#16556=CARTESIAN_POINT('Ctrl Pts',(-0.221794948880427,0.173254712590635,
12.8));
#16557=CARTESIAN_POINT('Ctrl Pts',(-0.213034382217665,0.185591542266393,
12.8));
#16558=CARTESIAN_POINT('Ctrl Pts',(-0.210424335567796,0.189267069455986,
12.8));
#16559=CARTESIAN_POINT('Ctrl Pts',(-0.207727064739911,0.192886342584116,
12.8));
#16560=CARTESIAN_POINT('Ctrl Pts',(-0.204952945248888,0.196435599584694,
12.8));
#16561=CARTESIAN_POINT('Ctrl Pts',(-0.194195780011085,0.210198504949868,
12.8));
#16562=CARTESIAN_POINT('Ctrl Pts',(-0.182257287796659,0.222952674257295,
12.8));
#16563=CARTESIAN_POINT('Ctrl Pts',(-0.169272003354721,0.23451832610712,
12.8));
#16564=CARTESIAN_POINT('Ctrl Pts',(-0.156757744220975,0.245664448084392,
12.8));
#16565=CARTESIAN_POINT('Ctrl Pts',(-0.143270367034069,0.255707981058576,
12.8));
#16566=CARTESIAN_POINT('Ctrl Pts',(-0.128892185405305,0.264462557919726,
12.8));
#16567=CARTESIAN_POINT('Origin',(-3.51939854619125E-17,1.42943244214557E-17,
12.8));
#16568=CARTESIAN_POINT('Origin',(0.,0.,0.));
#16569=CARTESIAN_POINT('Origin',(-0.144337567297407,-0.25,-0.6));
#16570=CARTESIAN_POINT('',(-0.144337567297407,-0.25,-0.6));
#16571=CARTESIAN_POINT('',(0.144337567297406,-0.25,-0.6));
#16572=CARTESIAN_POINT('',(-0.0721687836487033,-0.25,-0.6));
#16573=CARTESIAN_POINT('',(-0.144337567297407,-0.25,-0.3));
#16574=CARTESIAN_POINT('',(-0.144337567297407,-0.25,-0.6));
#16575=CARTESIAN_POINT('',(0.144337567297406,-0.25,-0.3));
#16576=CARTESIAN_POINT('',(-0.144337567297407,-0.25,-0.3));
#16577=CARTESIAN_POINT('',(0.144337567297406,-0.25,-0.6));
#16578=CARTESIAN_POINT('Origin',(-0.288675134594813,3.53525079574969E-17,
-0.6));
#16579=CARTESIAN_POINT('',(-0.288675134594813,3.53525079574969E-17,-0.6));
#16580=CARTESIAN_POINT('',(-0.252590742770461,-0.0625,-0.6));
#16581=CARTESIAN_POINT('',(-0.288675134594813,5.55111512312578E-17,-0.3));
#16582=CARTESIAN_POINT('',(-0.288675134594813,3.53525079574969E-17,-0.6));
#16583=CARTESIAN_POINT('',(-0.288675134594813,3.53525079574969E-17,-0.3));
#16584=CARTESIAN_POINT('Origin',(-0.144337567297406,0.25,-0.6));
#16585=CARTESIAN_POINT('',(-0.144337567297406,0.25,-0.6));
#16586=CARTESIAN_POINT('',(-0.180421959121758,0.1875,-0.6));
#16587=CARTESIAN_POINT('',(-0.144337567297406,0.25,-0.3));
#16588=CARTESIAN_POINT('',(-0.144337567297406,0.25,-0.6));
#16589=CARTESIAN_POINT('',(-0.144337567297406,0.25,-0.3));
#16590=CARTESIAN_POINT('Origin',(0.144337567297406,0.25,-0.6));
#16591=CARTESIAN_POINT('',(0.144337567297406,0.25,-0.6));
#16592=CARTESIAN_POINT('',(0.0721687836487033,0.25,-0.6));
#16593=CARTESIAN_POINT('',(0.144337567297406,0.25,-0.3));
#16594=CARTESIAN_POINT('',(0.144337567297406,0.25,-0.6));
#16595=CARTESIAN_POINT('',(0.144337567297406,0.25,-0.3));
#16596=CARTESIAN_POINT('Origin',(0.288675134594813,0.,-0.6));
#16597=CARTESIAN_POINT('',(0.288675134594813,0.,-0.6));
#16598=CARTESIAN_POINT('',(0.252590742770461,0.0625,-0.6));
#16599=CARTESIAN_POINT('',(0.288675134594813,0.,-0.3));
#16600=CARTESIAN_POINT('',(0.288675134594813,0.,-0.6));
#16601=CARTESIAN_POINT('',(0.288675134594813,0.,-0.3));
#16602=CARTESIAN_POINT('Origin',(0.144337567297406,-0.25,-0.6));
#16603=CARTESIAN_POINT('',(0.180421959121758,-0.1875,-0.6));
#16604=CARTESIAN_POINT('',(0.144337567297406,-0.25,-0.3));
#16605=CARTESIAN_POINT('Origin',(0.,0.,-0.3));
#16606=CARTESIAN_POINT('Origin',(0.,0.,0.));
#16607=CARTESIAN_POINT('',(-0.5,-6.12323399573677E-17,0.));
#16608=CARTESIAN_POINT('Origin',(0.,0.,0.));
#16609=CARTESIAN_POINT('Origin',(0.,0.,-0.6));
#16610=CARTESIAN_POINT('',(-0.5,-6.12323399573677E-17,-0.6));
#16611=CARTESIAN_POINT('',(-0.5,-6.12323399573677E-17,-0.6));
#16612=CARTESIAN_POINT('Origin',(0.,0.,-0.6));
#16613=CARTESIAN_POINT('Origin',(0.,0.,-0.6));
#16614=CARTESIAN_POINT('Origin',(0.,0.,13.6));
#16665=UNCERTAINTY_MEASURE_WITH_UNIT(LENGTH_MEASURE(0.001),#16688,
'DISTANCE_ACCURACY_VALUE',
'Maximum model space distance between geometric entities at asserted c
onnectivities');
#16666=UNCERTAINTY_MEASURE_WITH_UNIT(LENGTH_MEASURE(0.001),#16688,
'DISTANCE_ACCURACY_VALUE',
'Maximum model space distance between geometric entities at asserted c
onnectivities');
#16686=(
GEOMETRIC_REPRESENTATION_CONTEXT(3)
GLOBAL_UNCERTAINTY_ASSIGNED_CONTEXT((#16665))
GLOBAL_UNIT_ASSIGNED_CONTEXT((#16688,#16690,#16691))
REPRESENTATION_CONTEXT('','3D')
);
#16687=(
GEOMETRIC_REPRESENTATION_CONTEXT(3)
GLOBAL_UNCERTAINTY_ASSIGNED_CONTEXT((#16666))
GLOBAL_UNIT_ASSIGNED_CONTEXT((#16688,#16690,#16691))
REPRESENTATION_CONTEXT('','3D')
);
#16688=(
LENGTH_UNIT()
NAMED_UNIT(*)
SI_UNIT(.CENTI.,.METRE.)
);
#16690=(
NAMED_UNIT(*)
PLANE_ANGLE_UNIT()
SI_UNIT($,.RADIAN.)
);
#16691=(
NAMED_UNIT(*)
SI_UNIT($,.STERADIAN.)
SOLID_ANGLE_UNIT()
);
#16711=SHAPE_DEFINITION_REPRESENTATION(#16731,#16782);
#16731=PRODUCT_DEFINITION_SHAPE('',$,#16803);
#16782=SHAPE_REPRESENTATION('',(#6918),#16686);
#16783=PRODUCT_DEFINITION_CONTEXT('part definition',#16845,'design');
#16803=PRODUCT_DEFINITION('Socket head tie bolt M6x136',
'Socket head tie bolt M6x136',#16823,#16783);
#16823=PRODUCT_DEFINITION_FORMATION('',$,#16866);
#16845=APPLICATION_CONTEXT(
'Core Data for Automotive Mechanical Design Process');
#16846=PRODUCT_CONTEXT('part definition',#16845,'mechanical');
#16866=PRODUCT('Socket head tie bolt M6x136',
'Socket head tie bolt M6x136',$,(#16846));
#16881=PRESENTATION_STYLE_ASSIGNMENT((#16896));
#16896=SURFACE_STYLE_USAGE(.BOTH.,#16911);
#16911=SURFACE_SIDE_STYLE('',(#16926));
#16926=SURFACE_STYLE_FILL_AREA(#16941);
#16941=FILL_AREA_STYLE('Tie bolt gray',(#16956));
#16956=FILL_AREA_STYLE_COLOUR('Tie bolt gray',#16971);
#16971=COLOUR_RGB('Tie bolt gray',0.407843137254902,0.447058823529412,0.498039215686275);
ENDSEC;
END-ISO-10303-21;
